ISO-10303-21;
HEADER;
FILE_DESCRIPTION (('STEP AP214'),
    '1' );
FILE_NAME ('hex flange nut gradea_iso_ISO - 4161 - M5 - N.step',
    '2026-10-03T20:08:58',
    ( '' ),
    ( '' ),
    'SwSTEP 2.0',
    'SolidWorks 2026',
    '' );
FILE_SCHEMA (( 'AUTOMOTIVE_DESIGN' ));
ENDSEC;

DATA;
#16=CARTESIAN_POINT ( 'NONE',  ( -3.999999999999991562, -0.3979232138631201288, 7.067642911889882029E-15 ) ) ;
#25=CARTESIAN_POINT ( 'NONE',  ( 4.000000000000000000, -0.7890432684750908754, -0.04868663549882277369 ) ) ;
#34=ORIENTED_EDGE ( 'NONE', *, *, #4126, .T. ) ;
#36=CARTESIAN_POINT ( 'NONE',  ( -3.333333333333346804, 2.694301256218253560, -3.300726591567095358 ) ) ;
#38=VERTEX_POINT ( 'NONE', #7300 ) ;
#43=FILL_AREA_STYLE ('',( #2962 ) ) ;
#66=EDGE_LOOP ( 'NONE', ( #746, #6032, #7828, #1571 ) ) ;
#76=CARTESIAN_POINT ( 'NONE',  ( -2.000000000000008882, -3.464101615137750390, -8.673617379884035472E-15 ) ) ;
#84=CARTESIAN_POINT ( 'NONE',  ( 3.469446951953614189E-14, -3.469446951953614189E-15, -4.694516984716123886 ) ) ;
#91=LINE ( 'NONE', #9864, #6054 ) ;
#98=ORIENTED_EDGE ( 'NONE', *, *, #5230, .F. ) ;
#115=DIRECTION ( 'NONE',  ( 0.000000000000000000, -1.530455820933490821E-32, 1.000000000000000000 ) ) ;
#126=FACE_OUTER_BOUND ( 'NONE', #189, .T. ) ;
#157=DIRECTION ( 'NONE',  ( 0.000000000000000000, -1.530455820933490821E-32, 1.000000000000000000 ) ) ;
#159=ORIENTED_EDGE ( 'NONE', *, *, #9670, .T. ) ;
#166=EDGE_LOOP ( 'NONE', ( #3559, #613, #8519, #6620, #10979 ) ) ;
#173=ORIENTED_EDGE ( 'NONE', *, *, #5262, .T. ) ;
#176=FACE_OUTER_BOUND ( 'NONE', #7657, .T. ) ;
#177=CARTESIAN_POINT ( 'NONE',  ( 4.203935335434870524, 1.640780671294068238, -3.598452447879444627 ) ) ;
#180=CONICAL_SURFACE ( 'NONE', #8811, 4.000000000000000000, 0.8911886515913786111 ) ;
#182=CARTESIAN_POINT ( 'NONE',  ( 3.122502256758252770E-14, -4.862606272033112909, -3.745885042887444616 ) ) ;
#189=EDGE_LOOP ( 'NONE', ( #7813, #4813, #3733, #12234, #6794, #9118 ) ) ;
#214=CARTESIAN_POINT ( 'NONE',  ( 0.000000000000000000, 0.000000000000000000, 0.000000000000000000 ) ) ;
#222=VERTEX_POINT ( 'NONE', #588 ) ;
#227=( NAMED_UNIT ( * ) PLANE_ANGLE_UNIT ( ) SI_UNIT ( $, .RADIAN. ) );
#274=CARTESIAN_POINT ( 'NONE',  ( -3.999999999999628741, -1.658469974638250077, -3.531532913077053415 ) ) ;
#282=EDGE_LOOP ( 'NONE', ( #8241, #11601, #3963, #2292 ) ) ;
#295=DIRECTION ( 'NONE',  ( 0.000000000000000000, -1.530455820933490821E-32, 1.000000000000000000 ) ) ;
#308=ORIENTED_EDGE ( 'NONE', *, *, #4239, .F. ) ;
#313=CARTESIAN_POINT ( 'NONE',  ( -2.687328764639639544, 3.067272167851286646, -0.05923475698270460471 ) ) ;
#314=CARTESIAN_POINT ( 'NONE',  ( 3.436319922986161401, -2.634841920958475026, -3.531542292954823470 ) ) ;
#345=EDGE_CURVE ( 'NONE', #11393, #10993, #9909, .T. ) ;
#359=CARTESIAN_POINT ( 'NONE',  ( 0.1404048886732742751, 4.699864953788060795, -3.686887068327044048 ) ) ;
#360=EDGE_CURVE ( 'NONE', #9103, #2750, #9300, .T. ) ;
#370=EDGE_LOOP ( 'NONE', ( #12481, #7079, #9486, #1457, #9621, #6938, #4666 ) ) ;
#373=CARTESIAN_POINT ( 'NONE',  ( -0.6920835326022437561, -4.454600218803894229, -3.597382984111584303 ) ) ;
#376=CARTESIAN_POINT ( 'NONE',  ( 3.455068668934421883, -2.624017327439090774, -3.316620875263736057 ) ) ;
#384=PRESENTATION_STYLE_ASSIGNMENT (( #9321 ) ) ;
#389=CARTESIAN_POINT ( 'NONE',  ( 4.000000000000001776, -2.471525695159820124, -3.686886880705778413 ) ) ;
#394=CARTESIAN_POINT ( 'NONE',  ( 4.175002511812154538, 2.208363329454888113, -3.469254087858248514 ) ) ;
#402=( BOUNDED_SURFACE ( )  B_SPLINE_SURFACE ( 3, 2, ( 
 ( #8030, #7078, #2118 ),
 ( #6038, #5976, #6104 ),
 ( #8162, #6231, #12104 ),
 ( #10929, #10141, #1331 ),
 ( #1144, #2182, #12042 ),
 ( #5263, #5013, #10861 ) ),
 .UNSPECIFIED., .F., .F., .F. ) 
 B_SPLINE_SURFACE_WITH_KNOTS ( ( 4, 2, 4 ),
 ( 3, 3 ),
 ( 0.02032853247518126918, 0.02278863295364821906, 0.02524873343211516893 ),
 ( 0.000000000000000000, 1.000000000000000000 ),
 .UNSPECIFIED. ) 
 GEOMETRIC_REPRESENTATION_ITEM ( )  RATIONAL_B_SPLINE_SURFACE ( (
 ( 1.000000000000000000, 0.8047781615896838492, 1.000000000000000000),
 ( 1.000000000000000000, 0.8123767586288899167, 1.000000000000000000),
 ( 1.000000000000000000, 0.8190662415564865517, 1.000000000000000000),
 ( 1.000000000000000000, 0.8192361015668555568, 1.000000000000000000),
 ( 1.000000000000000000, 0.8126135807104249986, 1.000000000000000000),
 ( 1.000000000000000000, 0.8047712338318584457, 1.000000000000000000) ) ) 
 REPRESENTATION_ITEM ( '' )  SURFACE ( )  );
#404=CARTESIAN_POINT ( 'NONE',  ( 1.734723475976807094E-14, -3.469446951953614189E-15, -4.000000000000010658 ) ) ;
#408=CARTESIAN_POINT ( 'NONE',  ( 2.500000000000035527, -3.163285252166775924E-15, -4.974600000000009459 ) ) ;
#409=APPLICATION_CONTEXT ( 'automotive_design' ) ;
#413=ORIENTED_EDGE ( 'NONE', *, *, #5103, .T. ) ;
#417=EDGE_LOOP ( 'NONE', ( #3681, #5632, #1581, #10908 ) ) ;
#438=DIRECTION ( 'NONE',  ( 0.000000000000000000, -1.530455820933490821E-32, 1.000000000000000000 ) ) ;
#439=DIRECTION ( 'NONE',  ( -1.000000000000000000, 0.000000000000000000, 0.000000000000000000 ) ) ;
#447=( NAMED_UNIT ( * ) PLANE_ANGLE_UNIT ( ) SI_UNIT ( $, .RADIAN. ) );
#449=CARTESIAN_POINT ( 'NONE',  ( -3.999999999999994671, 0.000000000000000000, 8.673617379884035472E-15 ) ) ;
#458=CARTESIAN_POINT ( 'NONE',  ( 4.235886605889391809, 2.417314728048526984, -3.751161874094022686 ) ) ;
#487=CARTESIAN_POINT ( 'NONE',  ( 4.211140560182228043, -2.431303136016558231, -3.745885042887437510 ) ) ;
#497=ORIENTED_EDGE ( 'NONE', *, *, #10237, .F. ) ;
#506=ADVANCED_FACE ( 'NONE', ( #6248 ), #8873, .T. ) ;
#518=CARTESIAN_POINT ( 'NONE',  ( 4.000000000000001776, -0.8732470631450258702, -3.223155494240763197 ) ) ;
#524=CARTESIAN_POINT ( 'NONE',  ( 1.287237434361733213, 3.875615274277073308, -3.430618716626818276 ) ) ;
#529=VERTEX_POINT ( 'NONE', #2134 ) ;
#540=LINE ( 'NONE', #408, #11927 ) ;
#571=DIRECTION ( 'NONE',  ( 0.000000000000000000, 1.530455820933490821E-32, -1.000000000000000000 ) ) ;
#587=EDGE_LOOP ( 'NONE', ( #5195, #2640, #8200, #5319 ) ) ;
#588=CARTESIAN_POINT ( 'NONE',  ( 4.211140560182228043, -2.431303136016558231, -3.745885042887437510 ) ) ;
#595=DIRECTION ( 'NONE',  ( 0.8191520442889902442, 1.003171929053522775E-16, -0.5735764363510482688 ) ) ;
#599=CARTESIAN_POINT ( 'NONE',  ( -4.211140560182210280, 2.431303136016527144, -3.745885042887430405 ) ) ;
#613=ORIENTED_EDGE ( 'NONE', *, *, #6988, .F. ) ;
#641=CARTESIAN_POINT ( 'NONE',  ( -4.211140560182210280, 2.431303136016527144, -3.745885042887430405 ) ) ;
#655=CARTESIAN_POINT ( 'NONE',  ( 0.6920835326022525269, 4.454600218803853373, -3.597382984111599846 ) ) ;
#662=UNCERTAINTY_MEASURE_WITH_UNIT (LENGTH_MEASURE( 1.000000000000000082E-05 ), #8919, 'distance_accuracy_value', 'NONE');
#684=FACE_OUTER_BOUND ( 'NONE', #282, .T. ) ;
#691=FACE_OUTER_BOUND ( 'NONE', #7606, .T. ) ;
#693=CARTESIAN_POINT ( 'NONE',  ( 2.100000000000035172, -3.469446951953614189E-15, -5.000000000000011546 ) ) ;
#718=DIRECTION ( 'NONE',  ( 0.000000000000000000, -1.530455820933490821E-32, 1.000000000000000000 ) ) ;
#720=CARTESIAN_POINT ( 'NONE',  ( 0.3198814748697545451, 4.434118497892176158, -0.3507732604232445817 ) ) ;
#740=CIRCLE ( 'NONE', #11855, 2.499999999999999556 ) ;
#746=ORIENTED_EDGE ( 'NONE', *, *, #10417, .F. ) ;
#758=EDGE_CURVE ( 'NONE', #3906, #5156, #7358, .T. ) ;
#761=ORIENTED_EDGE ( 'NONE', *, *, #4308, .F. ) ;
#770=CARTESIAN_POINT ( 'NONE',  ( 0.000000000000000000, 0.000000000000000000, 0.000000000000000000 ) ) ;
#774=CARTESIAN_POINT ( 'NONE',  ( 4.000000000000001776, 2.309401076758487381, -3.433295621305364254 ) ) ;
#775=ORIENTED_EDGE ( 'NONE', *, *, #6278, .F. ) ;
#790=ORIENTED_EDGE ( 'NONE', *, *, #5569, .F. ) ;
#818=( BOUNDED_SURFACE ( )  B_SPLINE_SURFACE ( 3, 2, ( 
 ( #10960, #7111, #10048 ),
 ( #7993, #2286, #5236 ),
 ( #7303, #11097, #8193 ),
 ( #6136, #3327, #6262 ),
 ( #10173, #274, #11031 ),
 ( #9214, #4333, #12139 ) ),
 .UNSPECIFIED., .F., .F., .F. ) 
 B_SPLINE_SURFACE_WITH_KNOTS ( ( 4, 2, 4 ),
 ( 3, 3 ),
 ( 0.02027752710269158445, 0.02273781595091097299, 0.02519810479913036153 ),
 ( 0.000000000000000000, 1.000000000000000000 ),
 .UNSPECIFIED. ) 
 GEOMETRIC_REPRESENTATION_ITEM ( )  RATIONAL_B_SPLINE_SURFACE ( (
 ( 1.000000000000000000, 0.8047781431712808242, 1.000000000000000000),
 ( 1.000000000000000000, 0.8123773247083928561, 1.000000000000000000),
 ( 1.000000000000000000, 0.8190670192154906326, 1.000000000000000000),
 ( 1.000000000000000000, 0.8192353552912178261, 1.000000000000000000),
 ( 1.000000000000000000, 0.8126132098226828138, 1.000000000000000000),
 ( 1.000000000000000000, 0.8047712465856391439, 1.000000000000000000) ) ) 
 REPRESENTATION_ITEM ( '' )  SURFACE ( )  );
#830=DIRECTION ( 'NONE',  ( 0.8660254037844374864, -0.5000000000000018874, 7.395570986446984800E-31 ) ) ;
#833=CARTESIAN_POINT ( 'NONE',  ( 1.360585162435131057, -4.061296242128142886, -3.505054077164857951 ) ) ;
#841=CARTESIAN_POINT ( 'NONE',  ( 2.100000000000035172, -3.469446951953614189E-15, -4.694516984716123886 ) ) ;
#880=CARTESIAN_POINT ( 'NONE',  ( 3.469446951953614189E-14, -3.469446951953614189E-15, -5.000000000000011546 ) ) ;
#896=EDGE_CURVE ( 'NONE', #8586, #9298, #4700, .T. ) ;
#903=DIRECTION ( 'NONE',  ( 0.000000000000000000, -1.530455820933490821E-32, 1.000000000000000000 ) ) ;
#927=VERTEX_POINT ( 'NONE', #7131 ) ;
#939=FACE_OUTER_BOUND ( 'NONE', #66, .T. ) ;
#941=DIRECTION ( 'NONE',  ( -1.000000000000000000, 0.000000000000000000, 0.000000000000000000 ) ) ;
#945=CARTESIAN_POINT ( 'NONE',  ( 5.560781378645605955, -3.469446951953614189E-15, -4.000000000000010658 ) ) ;
#952=AXIS2_PLACEMENT_3D ( 'NONE', #4622, #4428, #10272 ) ;
#959=PLANE ( 'NONE',  #7403 ) ;
#962=VERTEX_POINT ( 'NONE', #5251 ) ;
#973=CARTESIAN_POINT ( 'NONE',  ( 0.000000000000000000, 0.000000000000000000, 0.000000000000000000 ) ) ;
#1005=CARTESIAN_POINT ( 'NONE',  ( 3.469446951953614189E-14, -3.469446951953614189E-15, -5.000000000000011546 ) ) ;
#1022=CARTESIAN_POINT ( 'NONE',  ( 0.6640947660595887259, -4.471078309994368283, -3.602146406945785806 ) ) ;
#1040=EDGE_LOOP ( 'NONE', ( #4220, #9747, #9061, #3791, #6995 ) ) ;
#1055=CARTESIAN_POINT ( 'NONE',  ( 5.603754474795991474E-15, 4.647089433458983621, -3.572167766733752359 ) ) ;
#1065=ORIENTED_EDGE ( 'NONE', *, *, #4126, .F. ) ;
#1069=CLOSED_SHELL ( 'NONE', ( #11145, #12631, #7196, #1644, #5684, #7981, #1755, #9394, #2322, #7154, #9459, #2680, #12532, #10758, #5653, #8693, #9274, #1388, #4949, #6562, #506, #1391, #8396, #5578, #8161, #6105, #5540, #7022, #10570, #4903, #4196, #11952 ) ) ;
#1078=PLANE ( 'NONE',  #5936 ) ;
#1079=ORIENTED_EDGE ( 'NONE', *, *, #5419, .F. ) ;
#1086=DIRECTION ( 'NONE',  ( 0.000000000000000000, -1.530455820933490821E-32, 1.000000000000000000 ) ) ;
#1113=CARTESIAN_POINT ( 'NONE',  ( 0.000000000000000000, 0.000000000000000000, 0.000000000000000000 ) ) ;
#1124=ORIENTED_EDGE ( 'NONE', *, *, #7748, .T. ) ;
#1137=AXIS2_PLACEMENT_3D ( 'NONE', #7402, #571, #10345 ) ;
#1144=CARTESIAN_POINT ( 'NONE',  ( -0.5449313310647205810, -4.304185902836956679, -3.316620875264007839 ) ) ;
#1147=CIRCLE ( 'NONE', #10169, 5.560781378645573980 ) ;
#1178=ORIENTED_EDGE ( 'NONE', *, *, #2514, .F. ) ;
#1208=B_SPLINE_CURVE_WITH_KNOTS ( 'NONE', 3,
 ( #8974, #4082, #8009, #36, #1248 ),
 .UNSPECIFIED., .F., .F.,
 ( 4, 1, 4 ),
 ( 0.000000000000000000, 0.002309401076758506657, 0.004618802153517013315 ),
 .UNSPECIFIED. ) ;
#1228=EDGE_CURVE ( 'NONE', #7688, #4329, #3065, .T. ) ;
#1248=CARTESIAN_POINT ( 'NONE',  ( -4.000000000000012434, 2.309401076758501592, -3.433295621305395340 ) ) ;
#1249=ORIENTED_EDGE ( 'NONE', *, *, #5103, .F. ) ;
#1269=CARTESIAN_POINT ( 'NONE',  ( 4.000000000000001776, 0.8378280264232703667, -3.220590601395643127 ) ) ;
#1271=CARTESIAN_POINT ( 'NONE',  ( -2.499999999999965805, -3.438830781974908945E-14, -5.000000000000011546 ) ) ;
#1274=CARTESIAN_POINT ( 'NONE',  ( 2.712762565639559309, -3.052587955997608127, -3.430618716626636200 ) ) ;
#1300=B_SPLINE_CURVE_WITH_KNOTS ( 'NONE', 3,
 ( #1871, #3628, #6587, #9582, #4651, #5549 ),
 .UNSPECIFIED., .F., .F.,
 ( 4, 2, 4 ),
 ( -3.640115492409309580E-06, 0.0002066546034003389619, 0.0004169493222930872466 ),
 .UNSPECIFIED. ) ;
#1303=DIRECTION ( 'NONE',  ( 1.000000000000000000, 0.000000000000000000, 0.000000000000000000 ) ) ;
#1331=CARTESIAN_POINT ( 'NONE',  ( -1.390230914382133642, -4.043987460488810193, -3.502507215260537432 ) ) ;
#1338=CARTESIAN_POINT ( 'NONE',  ( 0.000000000000000000, 4.862606272033057841, -3.745885042887454830 ) ) ;
#1355=FACE_OUTER_BOUND ( 'NONE', #587, .T. ) ;
#1380=CARTESIAN_POINT ( 'NONE',  ( -0.6448876103708466312, -4.246476118072349593, -0.2256878752776683428 ) ) ;
#1381=AXIS2_PLACEMENT_3D ( 'NONE', #1005, #11646, #2965 ) ;
#1388=ADVANCED_FACE ( 'NONE', ( #6497 ), #180, .T. ) ;
#1391=ADVANCED_FACE ( 'NONE', ( #9429 ), #10451, .T. ) ;
#1396=FACE_OUTER_BOUND ( 'NONE', #8792, .T. ) ;
#1457=ORIENTED_EDGE ( 'NONE', *, *, #8568, .F. ) ;
#1480=AXIS2_PLACEMENT_3D ( 'NONE', #10434, #3686, #5610 ) ;
#1482=CARTESIAN_POINT ( 'NONE',  ( 4.204115023516783012, -1.660442669500226565, -3.602151381774563177 ) ) ;
#1486=CARTESIAN_POINT ( 'NONE',  ( 0.5449313310647116992, 4.304185902836938915, -3.316620875263519341 ) ) ;
#1496=CARTESIAN_POINT ( 'NONE',  ( 0.000000000000000000, 4.862606272033057841, -3.745885042887454830 ) ) ;
#1533=LINE ( 'NONE', #693, #11840 ) ;
#1543=CARTESIAN_POINT ( 'NONE',  ( -0.3208286057739651032, 4.433571671609682241, -0.3503314178412564317 ) ) ;
#1544=CARTESIAN_POINT ( 'NONE',  ( 4.000000000000001776, -1.700175430507322449, -3.320327275037637804 ) ) ;
#1548=FACE_OUTER_BOUND ( 'NONE', #5567, .T. ) ;
#1564=CARTESIAN_POINT ( 'NONE',  ( 3.349226789952651107, 2.685125164760722605, -0.2236248678334721574 ) ) ;
#1566=CONICAL_SURFACE ( 'NONE', #8574, 4.000000000000000000, 0.8911886515913786111 ) ;
#1571=ORIENTED_EDGE ( 'NONE', *, *, #9670, .F. ) ;
#1581=ORIENTED_EDGE ( 'NONE', *, *, #5569, .T. ) ;
#1610=CARTESIAN_POINT ( 'NONE',  ( 1.734723475976807094E-14, -3.469446951953614189E-15, -4.000000000000010658 ) ) ;
#1611=VERTEX_POINT ( 'NONE', #9810 ) ;
#1616=CARTESIAN_POINT ( 'NONE',  ( 4.000000000000017764, -1.539600717839020527, -3.300726591567066492 ) ) ;
#1626=CARTESIAN_POINT ( 'NONE',  ( 3.679171394226029790, 2.494631558665822535, -0.3503314178412420543 ) ) ;
#1636=AXIS2_PLACEMENT_3D ( 'NONE', #7668, #2982, #8815 ) ;
#1644=ADVANCED_FACE ( 'NONE', ( #7002 ), #6361, .T. ) ;
#1664=MANIFOLD_SOLID_BREP ( 'EndChamfer', #1069 ) ;
#1700=CARTESIAN_POINT ( 'NONE',  ( 4.000000000000019540, -2.309401076758522464, -3.433295621305367806 ) ) ;
#1719=ORIENTED_EDGE ( 'NONE', *, *, #11169, .F. ) ;
#1720=EDGE_CURVE ( 'NONE', #2523, #10664, #12109, .T. ) ;
#1738=DIRECTION ( 'NONE',  ( 0.000000000000000000, -1.530455820933490821E-32, 1.000000000000000000 ) ) ;
#1742=CARTESIAN_POINT ( 'NONE',  ( -2.000000000000008882, -3.464101615137750390, -8.673617379884035472E-15 ) ) ;
#1755=ADVANCED_FACE ( 'NONE', ( #939 ), #3662, .F. ) ;
#1793=ORIENTED_EDGE ( 'NONE', *, *, #2345, .F. ) ;
#1798=CARTESIAN_POINT ( 'NONE',  ( -3.999999999999970690, -2.309401076758515359, -5.000000000000018652 ) ) ;
#1814=DIRECTION ( 'NONE',  ( 1.000000000000000000, 0.000000000000000000, 0.000000000000000000 ) ) ;
#1828=VERTEX_POINT ( 'NONE', #9680 ) ;
#1834=ORIENTED_EDGE ( 'NONE', *, *, #11321, .T. ) ;
#1861=CARTESIAN_POINT ( 'NONE',  ( 3.355112389629171243, -2.681727112203169838, -0.2256878752776775299 ) ) ;
#1862=EDGE_LOOP ( 'NONE', ( #7189, #9790, #12181 ) ) ;
#1870=ORIENTED_EDGE ( 'NONE', *, *, #1720, .T. ) ;
#1871=CARTESIAN_POINT ( 'NONE',  ( -4.211140560182161430, -2.431303136016561783, -3.745885042887451277 ) ) ;
#1875=DIRECTION ( 'NONE',  ( 1.000000000000000000, 0.000000000000000000, 0.000000000000000000 ) ) ;
#1896=DIRECTION ( 'NONE',  ( -0.9396926207859138680, 5.234467192292534210E-33, -0.3420201433256536139 ) ) ;
#1927=ORIENTED_EDGE ( 'NONE', *, *, #12089, .F. ) ;
#1938=CIRCLE ( 'NONE', #2995, 2.500000000000000888 ) ;
#1944=CARTESIAN_POINT ( 'NONE',  ( -3.999999999999994671, -2.309401076758511806, -0.4999999999999865663 ) ) ;
#1950=CARTESIAN_POINT ( 'NONE',  ( 3.122502256758252770E-14, -4.618802153517027165, -3.433295621305388678 ) ) ;
#1964=B_SPLINE_CURVE_WITH_KNOTS ( 'NONE', 3,
 ( #11740, #10820, #7865, #8828, #16, #4003 ),
 .UNSPECIFIED., .F., .F.,
 ( 4, 2, 4 ),
 ( 0.003358874760055555794, 0.004541967308452096383, 0.005725059856848637406 ),
 .UNSPECIFIED. ) ;
#2015=VERTEX_POINT ( 'NONE', #3214 ) ;
#2016=CARTESIAN_POINT ( 'NONE',  ( 4.197393957002303999, 7.389034437926038210E-14, -3.503767560748934251 ) ) ;
#2029=SURFACE_STYLE_USAGE ( .BOTH. , #8858 ) ;
#2071=DIRECTION ( 'NONE',  ( -1.000000000000000000, 0.000000000000000000, 0.000000000000000000 ) ) ;
#2077=EDGE_CURVE ( 'NONE', #12721, #8586, #4865, .T. ) ;
#2118=CARTESIAN_POINT ( 'NONE',  ( -4.235886605889374046, -2.417314728048561179, -3.751161874094032456 ) ) ;
#2121=DIRECTION ( 'NONE',  ( 0.000000000000000000, 0.000000000000000000, -1.000000000000000000 ) ) ;
#2124=AXIS2_PLACEMENT_3D ( 'NONE', #11803, #5926, #1875 ) ;
#2131=DIRECTION ( 'NONE',  ( 0.000000000000000000, -1.530455820933490821E-32, 1.000000000000000000 ) ) ;
#2134=CARTESIAN_POINT ( 'NONE',  ( 4.000000000000000000, 0.000000000000000000, 0.000000000000000000 ) ) ;
#2140=AXIS2_PLACEMENT_3D ( 'NONE', #10176, #7310, #7248 ) ;
#2152=DIRECTION ( 'NONE',  ( 0.000000000000000000, -1.530455820933490821E-32, 1.000000000000000000 ) ) ;
#2161=AXIS2_PLACEMENT_3D ( 'NONE', #8036, #7219, #7085 ) ;
#2170=VERTEX_POINT ( 'NONE', #841 ) ;
#2182=CARTESIAN_POINT ( 'NONE',  ( -0.5636800770139697159, -4.293361309318505903, -3.531542292955881734 ) ) ;
#2185=DIRECTION ( 'NONE',  ( 0.000000000000000000, -1.000000000000000000, -1.530455820933490821E-32 ) ) ;
#2200=DIRECTION ( 'NONE',  ( -0.8660254037844373753, 0.5000000000000021094, 0.000000000000000000 ) ) ;
#2211=DIRECTION ( 'NONE',  ( -0.000000000000000000, -1.530455820933490821E-32, 1.000000000000000000 ) ) ;
#2220=CONICAL_SURFACE ( 'NONE', #8179, 2.500000000000000888, 0.9599310885968785900 ) ;
#2223=FACE_OUTER_BOUND ( 'NONE', #5328, .T. ) ;
#2238=CARTESIAN_POINT ( 'NONE',  ( 4.204015924366190760, -1.626724848190935324, -3.610627190413396193 ) ) ;
#2253=CARTESIAN_POINT ( 'NONE',  ( 1.734723475976807094E-14, -3.469446951953614189E-15, -4.000000000000010658 ) ) ;
#2254=CARTESIAN_POINT ( 'NONE',  ( 4.141042297810618500, -2.227970268150431643, -3.687027686973626928 ) ) ;
#2264=SURFACE_STYLE_FILL_AREA ( #2456 ) ;
#2270=EDGE_CURVE ( 'NONE', #12673, #9454, #12708, .T. ) ;
#2271=CARTESIAN_POINT ( 'NONE',  ( -1.999999999999990008, -3.464101615137811230, -3.142992957459264325 ) ) ;
#2286=CARTESIAN_POINT ( 'NONE',  ( -3.999999999999992895, 1.677772373332863332, -3.535253723896553790 ) ) ;
#2287=DIRECTION ( 'NONE',  ( -1.000000000000000000, 0.000000000000000000, 0.000000000000000000 ) ) ;
#2292=ORIENTED_EDGE ( 'NONE', *, *, #2811, .F. ) ;
#2319=CARTESIAN_POINT ( 'NONE',  ( -3.355112389629172576, 2.681727112203154739, -0.2256878752776703412 ) ) ;
#2322=ADVANCED_FACE ( 'NONE', ( #6055 ), #5221, .T. ) ;
#2339=ORIENTED_EDGE ( 'NONE', *, *, #11234, .F. ) ;
#2345=EDGE_CURVE ( 'NONE', #927, #8673, #9017, .T. ) ;
#2357=B_SPLINE_CURVE_WITH_KNOTS ( 'NONE', 3,
 ( #4059, #12178, #11930, #10146, #2386, #8951, #10344, #1338 ),
 .UNSPECIFIED., .F., .F.,
 ( 4, 2, 2, 4 ),
 ( 0.000000000000000000, 0.002450665683189820563, 0.003675998524784731061, 0.004901331366379641993 ),
 .UNSPECIFIED. ) ;
#2361=ORIENTED_EDGE ( 'NONE', *, *, #4033, .T. ) ;
#2372=CARTESIAN_POINT ( 'NONE',  ( -4.175648173966062693, 2.207990556236520518, -3.469390959564077725 ) ) ;
#2375=CIRCLE ( 'NONE', #8106, 4.000000000000000000 ) ;
#2385=CARTESIAN_POINT ( 'NONE',  ( -4.000000000000001776, 2.309401076758498039, -0.4999999999999935052 ) ) ;
#2386=CARTESIAN_POINT ( 'NONE',  ( -1.393927851585486266, 4.043713361053526079, -3.526374918436849359 ) ) ;
#2414=CARTESIAN_POINT ( 'NONE',  ( 4.211140560182196069, 2.431303136016537358, -3.745885042887416638 ) ) ;
#2453=ORIENTED_EDGE ( 'NONE', *, *, #8794, .T. ) ;
#2456=FILL_AREA_STYLE ('',( #8245 ) ) ;
#2457=CARTESIAN_POINT ( 'NONE',  ( -4.197393957002295117, 0.4069871074557397939, -3.503767560748940468 ) ) ;
#2467=CARTESIAN_POINT ( 'NONE',  ( 4.000000000000001776, 2.309401076758487381, -3.433295621305364254 ) ) ;
#2498=CARTESIAN_POINT ( 'NONE',  ( 4.197393957002303999, -0.4069871074557490642, -3.503767560748930698 ) ) ;
#2511=ORIENTED_EDGE ( 'NONE', *, *, #9481, .F. ) ;
#2513=FACE_OUTER_BOUND ( 'NONE', #8088, .T. ) ;
#2514=EDGE_CURVE ( 'NONE', #11904, #38, #10573, .T. ) ;
#2523=VERTEX_POINT ( 'NONE', #10424 ) ;
#2534=CARTESIAN_POINT ( 'NONE',  ( 0.6810597143199710324, 4.461075778259524505, -3.598441714920695311 ) ) ;
#2567=CARTESIAN_POINT ( 'NONE',  ( 4.000000000000019540, -2.309401076758522464, -3.433295621305367806 ) ) ;
#2616=EDGE_CURVE ( 'NONE', #7775, #10242, #10236, .T. ) ;
#2617=DIRECTION ( 'NONE',  ( -1.000000000000000000, 1.224646799147356658E-16, 0.000000000000000000 ) ) ;
#2640=ORIENTED_EDGE ( 'NONE', *, *, #5125, .F. ) ;
#2641=CARTESIAN_POINT ( 'NONE',  ( 1.317756351988344399, -3.857995168970216326, -0.04852650426602535261 ) ) ;
#2667=CARTESIAN_POINT ( 'NONE',  ( 4.000000000000001776, 2.309401076758487381, -3.433295621305364254 ) ) ;
#2680=ADVANCED_FACE ( 'NONE', ( #9892 ), #1078, .T. ) ;
#2681=CARTESIAN_POINT ( 'NONE',  ( 3.469446951953614189E-14, -3.469446951953614189E-15, -5.000000000000011546 ) ) ;
#2682=AXIS2_PLACEMENT_3D ( 'NONE', #1610, #11414, #10295 ) ;
#2690=CARTESIAN_POINT ( 'NONE',  ( 5.384454397937153303, -3.469446951953614189E-15, -5.000000000000011546 ) ) ;
#2706=AXIS2_PLACEMENT_3D ( 'NONE', #8307, #8109, #2200 ) ;
#2715=CARTESIAN_POINT ( 'NONE',  ( -2.100000000000000089, -3.212271124132722995E-15, -0.2800830152838839626 ) ) ;
#2719=ORIENTED_EDGE ( 'NONE', *, *, #345, .F. ) ;
#2750=VERTEX_POINT ( 'NONE', #1271 ) ;
#2758=EDGE_CURVE ( 'NONE', #529, #9298, #10413, .T. ) ;
#2779=AXIS2_PLACEMENT_3D ( 'NONE', #84, #6070, #3950 ) ;
#2785=ORIENTED_EDGE ( 'NONE', *, *, #8568, .T. ) ;
#2797=EDGE_LOOP ( 'NONE', ( #1927, #10870, #9691, #1870, #6527 ) ) ;
#2811=EDGE_CURVE ( 'NONE', #3455, #4329, #11296, .T. ) ;
#2829=ORIENTED_EDGE ( 'NONE', *, *, #3369, .F. ) ;
#2846=VECTOR ( 'NONE', #3387, 1000.000000000000000 ) ;
#2856=ORIENTED_EDGE ( 'NONE', *, *, #3848, .F. ) ;
#2858=CARTESIAN_POINT ( 'NONE',  ( 0.5469614295418614436, -4.303013824935439047, -3.535263753545008658 ) ) ;
#2859=CARTESIAN_POINT ( 'NONE',  ( 2.499999999999999556, -4.715201491944146941E-33, 3.469446951953614189E-15 ) ) ;
#2909=AXIS2_PLACEMENT_3D ( 'NONE', #4053, #8942, #2927 ) ;
#2914=DIRECTION ( 'NONE',  ( 0.000000000000000000, -1.530455820933490821E-32, 1.000000000000000000 ) ) ;
#2927=DIRECTION ( 'NONE',  ( -1.000000000000000000, 0.000000000000000000, 0.000000000000000000 ) ) ;
#2934=CARTESIAN_POINT ( 'NONE',  ( 3.122502256758252770E-14, -4.618802153517027165, -3.433295621305388678 ) ) ;
#2935=DIRECTION ( 'NONE',  ( 0.000000000000000000, -1.530455820933490821E-32, 1.000000000000000000 ) ) ;
#2939=CARTESIAN_POINT ( 'NONE',  ( -4.000000000000022204, -1.344410693882025498E-14, -3.142992957459240344 ) ) ;
#2962=FILL_AREA_STYLE_COLOUR ( '', #8420 ) ;
#2965=DIRECTION ( 'NONE',  ( -1.000000000000000000, -1.243449787580175168E-14, 0.000000000000000000 ) ) ;
#2974=DIRECTION ( 'NONE',  ( -1.000000000000000000, 0.000000000000000000, 0.000000000000000000 ) ) ;
#2982=DIRECTION ( 'NONE',  ( -0.5000000000000016653, 0.8660254037844378194, -1.094764425253763580E-47 ) ) ;
#2995=AXIS2_PLACEMENT_3D ( 'NONE', #11807, #2935, #1814 ) ;
#3035=CARTESIAN_POINT ( 'NONE',  ( -3.999999999999991562, 2.309401076758501592, -4.999999999999993783 ) ) ;
#3065=LINE ( 'NONE', #5818, #4502 ) ;
#3100=CARTESIAN_POINT ( 'NONE',  ( 4.000000000000000888, 1.563622288139203453, -0.2253451193528330232 ) ) ;
#3106=CARTESIAN_POINT ( 'NONE',  ( 4.175648173966059140, -2.207990556236545832, -3.469390959564068400 ) ) ;
#3109=CARTESIAN_POINT ( 'NONE',  ( 4.211140560182196069, 2.431303136016537358, -3.745885042887416638 ) ) ;
#3120=CARTESIAN_POINT ( 'NONE',  ( -4.211140560182161430, -2.431303136016561783, -3.745885042887451277 ) ) ;
#3121=CARTESIAN_POINT ( 'NONE',  ( 3.469446951953614189E-14, -3.469446951953614189E-15, -4.694516984716123886 ) ) ;
#3129=( BOUNDED_SURFACE ( )  B_SPLINE_SURFACE ( 3, 2, ( 
 ( #6896, #12699, #9826 ),
 ( #7733, #2858, #1022 ),
 ( #8628, #6835, #833 ),
 ( #3744, #1274, #5021 ),
 ( #376, #314, #6238 ),
 ( #3106, #2254, #9895 ) ),
 .UNSPECIFIED., .F., .F., .F. ) 
 B_SPLINE_SURFACE_WITH_KNOTS ( ( 4, 2, 4 ),
 ( 3, 3 ),
 ( 0.02032853247518126918, 0.02278863295364821906, 0.02524873343211517240 ),
 ( 0.000000000000000000, 1.000000000000000000 ),
 .UNSPECIFIED. ) 
 GEOMETRIC_REPRESENTATION_ITEM ( )  RATIONAL_B_SPLINE_SURFACE ( (
 ( 1.000000000000000000, 0.8047781615896836271, 1.000000000000000000),
 ( 1.000000000000000000, 0.8123767586288546116, 1.000000000000000000),
 ( 1.000000000000000000, 0.8190662415565334031, 1.000000000000000000),
 ( 1.000000000000000000, 0.8192361015668073732, 1.000000000000000000),
 ( 1.000000000000000000, 0.8126135807104617470, 1.000000000000000000),
 ( 1.000000000000000000, 0.8047712338318590009, 1.000000000000000000) ) ) 
 REPRESENTATION_ITEM ( '' )  SURFACE ( )  );
#3151=EDGE_LOOP ( 'NONE', ( #12169, #9101, #10311, #1178, #8918 ) ) ;
#3189=VECTOR ( 'NONE', #7621, 1000.000000000000000 ) ;
#3190=LINE ( 'NONE', #5169, #6207 ) ;
#3212=SHAPE_DEFINITION_REPRESENTATION ( #12249, #9199 ) ;
#3214=CARTESIAN_POINT ( 'NONE',  ( -3.999999999999963585, -2.309401076758515359, -3.433295621305398893 ) ) ;
#3222=CARTESIAN_POINT ( 'NONE',  ( -1.243802165048778496, 3.900692638707451643, -3.223146290109630829 ) ) ;
#3227=EDGE_LOOP ( 'NONE', ( #5568, #775, #11039 ) ) ;
#3228=ORIENTED_EDGE ( 'NONE', *, *, #5969, .T. ) ;
#3240=CONICAL_SURFACE ( 'NONE', #12283, 2.059999999999998721, 0.9599310885968738161 ) ;
#3246=CARTESIAN_POINT ( 'NONE',  ( -3.999999999999991562, 0.3987449864459988169, -0.01220643443059140493 ) ) ;
#3282=CARTESIAN_POINT ( 'NONE',  ( -0.5469614295415836658, 4.303013824935630893, -3.535263753544197751 ) ) ;
#3289=EDGE_CURVE ( 'NONE', #1611, #10248, #9311, .T. ) ;
#3327=CARTESIAN_POINT ( 'NONE',  ( -3.999999999999993339, -0.8232339106130704964, -3.430630286862755174 ) ) ;
#3342=CARTESIAN_POINT ( 'NONE',  ( -3.455068668934444087, 2.624017327439054359, -3.316620875263493584 ) ) ;
#3354=B_SPLINE_CURVE_WITH_KNOTS ( 'NONE', 3,
 ( #4721, #8651, #3698, #1564, #1626, #5500 ),
 .UNSPECIFIED., .F., .F.,
 ( 4, 2, 4 ),
 ( 0.002365888236227993349, 0.003551327329835085415, 0.004736766423442177049 ),
 .UNSPECIFIED. ) ;
#3357=CARTESIAN_POINT ( 'NONE',  ( -2.449848172108533007, -3.432307619358755169, -3.503702292528917628 ) ) ;
#3369=EDGE_CURVE ( 'NONE', #12673, #4184, #10547, .T. ) ;
#3371=CARTESIAN_POINT ( 'NONE',  ( -3.999999999999991562, 0.9868501483902569760, -0.09357334158578810290 ) ) ;
#3387=DIRECTION ( 'NONE',  ( 0.000000000000000000, -1.530455820933490821E-32, 1.000000000000000000 ) ) ;
#3396=VERTEX_POINT ( 'NONE', #6279 ) ;
#3455=VERTEX_POINT ( 'NONE', #2690 ) ;
#3490=CARTESIAN_POINT ( 'NONE',  ( -0.6507732100473482273, 4.243078065514778174, -0.2236248678334831208 ) ) ;
#3495=CARTESIAN_POINT ( 'NONE',  ( 4.000000000000000000, 2.309401076758511806, -0.5000000000000038858 ) ) ;
#3507=CARTESIAN_POINT ( 'NONE',  ( 0.6448876103708305330, 4.246476118072349593, -0.2256878752776663444 ) ) ;
#3515=EDGE_CURVE ( 'NONE', #12512, #12721, #6407, .T. ) ;
#3527=VERTEX_POINT ( 'NONE', #7562 ) ;
#3538=CARTESIAN_POINT ( 'NONE',  ( 0.000000000000000000, 0.000000000000000000, 0.000000000000000000 ) ) ;
#3555=CARTESIAN_POINT ( 'NONE',  ( -4.204015924366180101, 1.626724848190912898, -3.610627190413403742 ) ) ;
#3557=CARTESIAN_POINT ( 'NONE',  ( 3.469446951953614189E-14, -3.469446951953614189E-15, -5.000000000000011546 ) ) ;
#3559=ORIENTED_EDGE ( 'NONE', *, *, #5077, .T. ) ;
#3563=EDGE_CURVE ( 'NONE', #2750, #11393, #10703, .T. ) ;
#3564=AXIS2_PLACEMENT_3D ( 'NONE', #8227, #11128, #6229 ) ;
#3623=FACE_OUTER_BOUND ( 'NONE', #6081, .T. ) ;
#3628=CARTESIAN_POINT ( 'NONE',  ( -4.154094228333783612, -2.398367420967604247, -3.721909803043274234 ) ) ;
#3636=LINE ( 'NONE', #12523, #3189 ) ;
#3637=EDGE_CURVE ( 'NONE', #2170, #3527, #8302, .T. ) ;
#3662=CYLINDRICAL_SURFACE ( 'NONE', #3900, 2.100000000000000089 ) ;
#3667=CARTESIAN_POINT ( 'NONE',  ( 3.469446951953614189E-14, -3.469446951953614189E-15, -4.974600000000009459 ) ) ;
#3680=PLANE ( 'NONE',  #1636 ) ;
#3681=ORIENTED_EDGE ( 'NONE', *, *, #3369, .T. ) ;
#3683=DIRECTION ( 'NONE',  ( 0.000000000000000000, -1.530455820933490821E-32, 1.000000000000000000 ) ) ;
#3686=DIRECTION ( 'NONE',  ( 0.000000000000000000, 1.530455820933490821E-32, -1.000000000000000000 ) ) ;
#3693=CARTESIAN_POINT ( 'NONE',  ( 0.000000000000000000, 0.000000000000000000, 3.469446951953614189E-15 ) ) ;
#3695=CARTESIAN_POINT ( 'NONE',  ( 1.828356344711636217, 3.563200125723174239, 6.226539195266360215E-15 ) ) ;
#3696=CARTESIAN_POINT ( 'NONE',  ( 0.6937372685066846012, -4.453844082567727902, -3.610536846335899774 ) ) ;
#3698=CARTESIAN_POINT ( 'NONE',  ( 2.682243648011664039, 3.070208061305297775, -0.04852650426600636779 ) ) ;
#3703=ORIENTED_EDGE ( 'NONE', *, *, #5230, .T. ) ;
#3729=DIRECTION ( 'NONE',  ( 0.000000000000000000, 1.530455820933490821E-32, -1.000000000000000000 ) ) ;
#3733=ORIENTED_EDGE ( 'NONE', *, *, #7689, .F. ) ;
#3744=CARTESIAN_POINT ( 'NONE',  ( 2.725741868436138304, -3.045094352033984375, -3.220599429844055894 ) ) ;
#3768=AXIS2_PLACEMENT_3D ( 'NONE', #3035, #2974, #2914 ) ;
#3791=ORIENTED_EDGE ( 'NONE', *, *, #2616, .T. ) ;
#3806=CARTESIAN_POINT ( 'NONE',  ( -0.1410422978106043723, 4.700232962125088676, -3.687027686973631813 ) ) ;
#3840=B_SPLINE_CURVE_WITH_KNOTS ( 'NONE', 3,
 ( #2385, #5331, #2319, #11004, #313, #12177, #6109, #10145 ),
 .UNSPECIFIED., .F., .F.,
 ( 4, 2, 2, 4 ),
 ( 2.465131517029315700E-07, 0.001183067374689838287, 0.001774477805458905951, 0.002365888236227973833 ),
 .UNSPECIFIED. ) ;
#3848=EDGE_CURVE ( 'NONE', #9454, #7175, #7483, .T. ) ;
#3868=B_SPLINE_CURVE_WITH_KNOTS ( 'NONE', 3,
 ( #4001, #4193, #2271, #6188, #4320 ),
 .UNSPECIFIED., .F., .F.,
 ( 4, 1, 4 ),
 ( 0.000000000000000000, 0.002309401076758505790, 0.004618802153517011580 ),
 .UNSPECIFIED. ) ;
#3894=CARTESIAN_POINT ( 'NONE',  ( 0.000000000000000000, 0.000000000000000000, -0.3080913168122742518 ) ) ;
#3900=AXIS2_PLACEMENT_3D ( 'NONE', #4871, #7833, #4684 ) ;
#3906=VERTEX_POINT ( 'NONE', #9464 ) ;
#3924=CARTESIAN_POINT ( 'NONE',  ( 4.000000000000000000, -2.309401076758518911, -0.4999999999999917843 ) ) ;
#3929=DIRECTION ( 'NONE',  ( 0.5000000000000013323, -0.8660254037844379305, 7.395570986446986770E-32 ) ) ;
#3934=( LENGTH_UNIT ( ) NAMED_UNIT ( * ) SI_UNIT ( .MILLI., .METRE. ) );
#3950=DIRECTION ( 'NONE',  ( -1.000000000000000000, 0.000000000000000000, 0.000000000000000000 ) ) ;
#3963=ORIENTED_EDGE ( 'NONE', *, *, #4068, .F. ) ;
#3971=PRESENTATION_STYLE_ASSIGNMENT (( #2029 ) ) ;
#3976=DIRECTION ( 'NONE',  ( 0.000000000000000000, 1.530455820933490821E-32, -1.000000000000000000 ) ) ;
#4001=CARTESIAN_POINT ( 'NONE',  ( -3.999999999999963585, -2.309401076758515359, -3.433295621305398893 ) ) ;
#4003=CARTESIAN_POINT ( 'NONE',  ( -3.999999999999994671, 0.000000000000000000, 8.673617379884035472E-15 ) ) ;
#4010=AXIS2_PLACEMENT_3D ( 'NONE', #8594, #12539, #7698 ) ;
#4023=CARTESIAN_POINT ( 'NONE',  ( -3.976033822569857420E-13, 4.796734841935179183, -3.721909803043276455 ) ) ;
#4030=ORIENTED_EDGE ( 'NONE', *, *, #7363, .T. ) ;
#4033=EDGE_CURVE ( 'NONE', #8673, #3906, #3840, .T. ) ;
#4041=DIRECTION ( 'NONE',  ( 0.000000000000000000, 1.530455820933490821E-32, -1.000000000000000000 ) ) ;
#4053=CARTESIAN_POINT ( 'NONE',  ( 0.000000000000000000, 4.618802153517009401, -1.040834085586084257E-14 ) ) ;
#4057=CARTESIAN_POINT ( 'NONE',  ( 2.059999999999998721, 0.000000000000000000, -0.3080913168122742518 ) ) ;
#4058=CARTESIAN_POINT ( 'NONE',  ( 0.000000000000000000, 0.000000000000000000, 0.000000000000000000 ) ) ;
#4059=CARTESIAN_POINT ( 'NONE',  ( -4.211140560182210280, 2.431303136016527144, -3.745885042887430405 ) ) ;
#4068=EDGE_CURVE ( 'NONE', #4329, #10248, #12014, .T. ) ;
#4082=CARTESIAN_POINT ( 'NONE',  ( -0.6666666666666659635, 4.233901974057234341, -3.300726591567097579 ) ) ;
#4096=( GEOMETRIC_REPRESENTATION_CONTEXT ( 3 ) GLOBAL_UNCERTAINTY_ASSIGNED_CONTEXT ( ( #662 ) ) GLOBAL_UNIT_ASSIGNED_CONTEXT ( ( #8919, #227, #5192 ) ) REPRESENTATION_CONTEXT ( 'NONE', 'WORKASPACE' ) );
#4100=ORIENTED_EDGE ( 'NONE', *, *, #10552, .T. ) ;
#4112=CARTESIAN_POINT ( 'NONE',  ( -1.391697335622786857, -4.043246145443387896, -3.503898532754379680 ) ) ;
#4119=CARTESIAN_POINT ( 'NONE',  ( 4.101954839143195919, 2.368264730583003352, -3.681130640444369106 ) ) ;
#4126=EDGE_CURVE ( 'NONE', #10385, #8996, #6466, .T. ) ;
#4129=CARTESIAN_POINT ( 'NONE',  ( -2.344047193898590287, -3.265465875126468021, -6.784733907506943744E-16 ) ) ;
#4152=CARTESIAN_POINT ( 'NONE',  ( 0.000000000000000000, -3.469446951953614189E-14, -25.03750572909320837 ) ) ;
#4173=FACE_BOUND ( 'NONE', #8027, .T. ) ;
#4184=VERTEX_POINT ( 'NONE', #2715 ) ;
#4193=CARTESIAN_POINT ( 'NONE',  ( -3.333333333333297954, -2.694301256218267326, -3.300726591567099355 ) ) ;
#4196=ADVANCED_FACE ( 'NONE', ( #691 ), #2220, .F. ) ;
#4209=CONICAL_SURFACE ( 'NONE', #12450, 4.000000000000000000, 0.8911886515913786111 ) ;
#4220=ORIENTED_EDGE ( 'NONE', *, *, #10680, .F. ) ;
#4239=EDGE_CURVE ( 'NONE', #10242, #2523, #9974, .T. ) ;
#4272=CARTESIAN_POINT ( 'NONE',  ( -4.000000000000001776, 2.309401076758498039, -0.4999999999999935052 ) ) ;
#4288=CARTESIAN_POINT ( 'NONE',  ( -2.725741868436132531, 3.045094352033964835, -3.220599429844243300 ) ) ;
#4297=FACE_OUTER_BOUND ( 'NONE', #6825, .T. ) ;
#4304=DIRECTION ( 'NONE',  ( 0.000000000000000000, 1.530455820933490821E-32, -1.000000000000000000 ) ) ;
#4308=EDGE_CURVE ( 'NONE', #2750, #9103, #6745, .T. ) ;
#4320=CARTESIAN_POINT ( 'NONE',  ( 3.122502256758252770E-14, -4.618802153517027165, -3.433295621305388678 ) ) ;
#4329=VERTEX_POINT ( 'NONE', #945 ) ;
#4333=CARTESIAN_POINT ( 'NONE',  ( -3.999999999999993339, -2.472261339043345885, -3.687027428081202540 ) ) ;
#4347=CARTESIAN_POINT ( 'NONE',  ( -1.312671235360375999, -3.860931062424216798, -0.05923475698270382062 ) ) ;
#4360=EDGE_CURVE ( 'NONE', #1611, #3455, #7741, .T. ) ;
#4380=CARTESIAN_POINT ( 'NONE',  ( -4.000000000000001776, 2.309401076758498039, -0.4999999999999935052 ) ) ;
#4389=B_SPLINE_CURVE_WITH_KNOTS ( 'NONE', 3,
 ( #9662, #10699, #2939, #4603, #8518 ),
 .UNSPECIFIED., .F., .F.,
 ( 4, 1, 4 ),
 ( 0.000000000000000000, 0.002309401076758505790, 0.004618802153517011580 ),
 .UNSPECIFIED. ) ;
#4390=CARTESIAN_POINT ( 'NONE',  ( 3.540020015735469983, 2.810662092924230304, -3.602146406945803125 ) ) ;
#4411=TOROIDAL_SURFACE ( 'NONE', #2140, 5.384454397937118664, 0.5155456020628804703 ) ;
#4428=DIRECTION ( 'NONE',  ( 0.000000000000000000, -1.530455820933490821E-32, 1.000000000000000000 ) ) ;
#4439=PRODUCT_DEFINITION_CONTEXT ( 'detailed design', #5674, 'design' ) ;
#4445=( NAMED_UNIT ( * ) SI_UNIT ( $, .STERADIAN. ) SOLID_ANGLE_UNIT ( ) );
#4446=CARTESIAN_POINT ( 'NONE',  ( -4.207491450040580894, 2.029819825146461199, -3.671670828759564742 ) ) ;
#4447=CARTESIAN_POINT ( 'NONE',  ( -1.317756351988342400, 3.857995168970202116, -0.04852650426601479161 ) ) ;
#4449=CARTESIAN_POINT ( 'NONE',  ( 4.000000000000002665, -0.8578082829537354570, -3.433262215449998322 ) ) ;
#4454=CARTESIAN_POINT ( 'NONE',  ( 0.5636800770131545901, 4.293361309317545782, -3.531542292954619633 ) ) ;
#4465=CARTESIAN_POINT ( 'NONE',  ( 3.861362476283253464, 2.629030857715976222, -3.671615880910352292 ) ) ;
#4502=VECTOR ( 'NONE', #8839, 1000.000000000000227 ) ;
#4505=DIRECTION ( 'NONE',  ( -0.000000000000000000, 1.530455820933490821E-32, -1.000000000000000000 ) ) ;
#4527=CARTESIAN_POINT ( 'NONE',  ( 4.000000000000019540, -2.309401076758522464, -3.433295621305367806 ) ) ;
#4532=CARTESIAN_POINT ( 'NONE',  ( 2.500000000000000444, -3.469446951953614189E-14, -25.03750572909320837 ) ) ;
#4541=ORIENTED_EDGE ( 'NONE', *, *, #10166, .F. ) ;
#4542=EDGE_CURVE ( 'NONE', #3396, #8673, #7006, .T. ) ;
#4547=DIRECTION ( 'NONE',  ( 1.224646799147353207E-16, 1.000000000000000000, 1.530455820933490821E-32 ) ) ;
#4554=MECHANICAL_DESIGN_GEOMETRIC_PRESENTATION_REPRESENTATION('',(#8033),#5361);
#4597=CARTESIAN_POINT ( 'NONE',  ( 1.391697335622807952, 4.043246145443367467, -3.503898532754372130 ) ) ;
#4602=DIRECTION ( 'NONE',  ( 0.000000000000000000, -1.530455820933490821E-32, 1.000000000000000000 ) ) ;
#4603=CARTESIAN_POINT ( 'NONE',  ( -3.999999999999964473, -1.539600717839013422, -3.300726591567098023 ) ) ;
#4622=CARTESIAN_POINT ( 'NONE',  ( 3.469446951953614189E-14, -3.469446951953614189E-15, -4.484454397937126302 ) ) ;
#4647=FACE_OUTER_BOUND ( 'NONE', #9678, .T. ) ;
#4651=CARTESIAN_POINT ( 'NONE',  ( -3.999999999999963585, -2.309401076758515359, -3.504269196027888889 ) ) ;
#4666=ORIENTED_EDGE ( 'NONE', *, *, #5125, .T. ) ;
#4667=CARTESIAN_POINT ( 'NONE',  ( 0.6666666666666951624, -4.233901974057275197, -3.300726591567086921 ) ) ;
#4684=DIRECTION ( 'NONE',  ( 1.000000000000000000, 0.000000000000000000, 0.000000000000000000 ) ) ;
#4687=DIRECTION ( 'NONE',  ( 0.000000000000000000, 1.530455820933490821E-32, -1.000000000000000000 ) ) ;
#4692=UNCERTAINTY_MEASURE_WITH_UNIT (LENGTH_MEASURE( 1.000000000000000082E-05 ), #10289, 'distance_accuracy_value', 'NONE');
#4694=VERTEX_POINT ( 'NONE', #9479 ) ;
#4700=LINE ( 'NONE', #6092, #9842 ) ;
#4702=DIRECTION ( 'NONE',  ( 0.000000000000000000, -1.530455820933490821E-32, 1.000000000000000000 ) ) ;
#4708=CYLINDRICAL_SURFACE ( 'NONE', #10730, 2.500000000000000444 ) ;
#4721=CARTESIAN_POINT ( 'NONE',  ( 2.000000000000007105, 3.464101615137750390, 6.938893903907228378E-15 ) ) ;
#4748=AXIS2_PLACEMENT_3D ( 'NONE', #7467, #4505, #5471 ) ;
#4774=LINE ( 'NONE', #10499, #5551 ) ;
#4782=CARTESIAN_POINT ( 'NONE',  ( -7.557654583407860981E-15, -4.647091401871400684, -3.572172305156889660 ) ) ;
#4801=DIRECTION ( 'NONE',  ( -1.000000000000000000, 0.000000000000000000, 0.000000000000000000 ) ) ;
#4813=ORIENTED_EDGE ( 'NONE', *, *, #8251, .F. ) ;
#4821=ORIENTED_EDGE ( 'NONE', *, *, #7689, .T. ) ;
#4837=DIRECTION ( 'NONE',  ( 1.000000000000000000, 0.000000000000000000, 0.000000000000000000 ) ) ;
#4847=CARTESIAN_POINT ( 'NONE',  ( -2.099999999999965450, -3.212271124132670141E-15, -5.000000000000011546 ) ) ;
#4865=B_SPLINE_CURVE_WITH_KNOTS ( 'NONE', 3,
 ( #4527, #1616, #11485, #6458, #2667 ),
 .UNSPECIFIED., .F., .F.,
 ( 4, 1, 4 ),
 ( 0.000000000000000000, 0.002309401076758506657, 0.004618802153517013315 ),
 .UNSPECIFIED. ) ;
#4871=CARTESIAN_POINT ( 'NONE',  ( 3.469446951953614189E-14, -3.469446951953614189E-15, -5.000000000000011546 ) ) ;
#4889=PLANE ( 'NONE',  #3768 ) ;
#4890=ORIENTED_EDGE ( 'NONE', *, *, #896, .T. ) ;
#4891=CARTESIAN_POINT ( 'NONE',  ( 2.345747346278117096, -3.264484291692501206, -0.01223254789874552578 ) ) ;
#4897=CARTESIAN_POINT ( 'NONE',  ( 0.000000000000000000, -4.618802153517027165, -5.000000000000000888 ) ) ;
#4901=LINE ( 'NONE', #7859, #11364 ) ;
#4903=ADVANCED_FACE ( 'NONE', ( #5944 ), #3240, .F. ) ;
#4911=B_SPLINE_CURVE_WITH_KNOTS ( 'NONE', 3,
 ( #2467, #5354, #5417, #7422, #9271 ),
 .UNSPECIFIED., .F., .F.,
 ( 4, 1, 4 ),
 ( 0.000000000000000000, 0.002309401076758506657, 0.004618802153517013315 ),
 .UNSPECIFIED. ) ;
#4948=VECTOR ( 'NONE', #12642, 999.9999999999998863 ) ;
#4949=ADVANCED_FACE ( 'NONE', ( #10113 ), #1566, .T. ) ;
#4971=CARTESIAN_POINT ( 'NONE',  ( 3.469446951953614189E-14, -3.469446951953614189E-15, -5.000000000000011546 ) ) ;
#4973=CARTESIAN_POINT ( 'NONE',  ( -3.349226789952653327, -2.685125164760732375, -0.2236248678334778750 ) ) ;
#4981=DIRECTION ( 'NONE',  ( 0.000000000000000000, -1.530455820933490821E-32, 1.000000000000000000 ) ) ;
#5007=B_SPLINE_CURVE_WITH_KNOTS ( 'NONE', 3,
 ( #599, #9346, #11237, #6271, #6333, #6403 ),
 .UNSPECIFIED., .F., .F.,
 ( 4, 2, 4 ),
 ( -3.640115492410384041E-06, 0.0002066546034003272525, 0.0004169493222930648578 ),
 .UNSPECIFIED. ) ;
#5013=CARTESIAN_POINT ( 'NONE',  ( 0.1410422978106194436, -4.700232962125120650, -3.687027686973640694 ) ) ;
#5021=CARTESIAN_POINT ( 'NONE',  ( 2.807080416178990845, -3.225969019225313872, -3.502507215260560969 ) ) ;
#5044=CONICAL_SURFACE ( 'NONE', #1137, 4.000000000000000000, 0.8911886515913786111 ) ;
#5051=DIRECTION ( 'NONE',  ( 0.000000000000000000, 1.530455820933490821E-32, -1.000000000000000000 ) ) ;
#5071=AXIS2_PLACEMENT_3D ( 'NONE', #6952, #4041, #8230 ) ;
#5077=EDGE_CURVE ( 'NONE', #12721, #222, #5866, .T. ) ;
#5103=EDGE_CURVE ( 'NONE', #9103, #10993, #5298, .T. ) ;
#5125=EDGE_CURVE ( 'NONE', #4694, #962, #8173, .T. ) ;
#5145=CARTESIAN_POINT ( 'NONE',  ( 4.000000000000000000, 2.309401076758511806, -0.5000000000000038858 ) ) ;
#5156=VERTEX_POINT ( 'NONE', #9215 ) ;
#5169=CARTESIAN_POINT ( 'NONE',  ( -2.499999999999966249, -3.469446951953614189E-15, -4.974600000000009459 ) ) ;
#5192=( NAMED_UNIT ( * ) SI_UNIT ( $, .STERADIAN. ) SOLID_ANGLE_UNIT ( ) );
#5195=ORIENTED_EDGE ( 'NONE', *, *, #10728, .T. ) ;
#5206=CARTESIAN_POINT ( 'NONE',  ( 4.000000000000001776, 1.680228229147209040, -3.316631783031879444 ) ) ;
#5221=PLANE ( 'NONE',  #2706 ) ;
#5230=EDGE_CURVE ( 'NONE', #222, #10385, #10468, .T. ) ;
#5233=ORIENTED_EDGE ( 'NONE', *, *, #6278, .T. ) ;
#5236=CARTESIAN_POINT ( 'NONE',  ( -4.204114297095544295, 1.660363174096594951, -3.602136431857922982 ) ) ;
#5251=CARTESIAN_POINT ( 'NONE',  ( 4.211140560182196069, 2.431303136016537358, -3.745885042887416638 ) ) ;
#5254=CARTESIAN_POINT ( 'NONE',  ( 4.197393957002303999, 7.389034437926038210E-14, -3.503767560748934251 ) ) ;
#5262=EDGE_CURVE ( 'NONE', #12512, #10385, #6161, .T. ) ;
#5263=CARTESIAN_POINT ( 'NONE',  ( 0.1756481739660588626, -4.720212674039006906, -3.469390959564082166 ) ) ;
#5298=LINE ( 'NONE', #4532, #2846 ) ;
#5310=CARTESIAN_POINT ( 'NONE',  ( -1.144235203016672475, -3.958177651039087586, -0.09382832055445461394 ) ) ;
#5319=ORIENTED_EDGE ( 'NONE', *, *, #10552, .F. ) ;
#5328=EDGE_LOOP ( 'NONE', ( #6049, #9961, #7266, #5505 ) ) ;
#5331=CARTESIAN_POINT ( 'NONE',  ( -3.680118525130247509, 2.494084732383328173, -0.3507732604232469131 ) ) ;
#5352=ORIENTED_EDGE ( 'NONE', *, *, #2077, .T. ) ;
#5354=CARTESIAN_POINT ( 'NONE',  ( 3.333333333333334814, 2.694301256218240237, -3.300726591567062940 ) ) ;
#5361=( GEOMETRIC_REPRESENTATION_CONTEXT ( 3 ) GLOBAL_UNCERTAINTY_ASSIGNED_CONTEXT ( ( #4692 ) ) GLOBAL_UNIT_ASSIGNED_CONTEXT ( ( #10289, #8306, #4445 ) ) REPRESENTATION_CONTEXT ( 'NONE', 'WORKASPACE' ) );
#5362=CARTESIAN_POINT ( 'NONE',  ( 3.469446951953614189E-15, 4.618802153517009401, -0.5000000000000091038 ) ) ;
#5363=CARTESIAN_POINT ( 'NONE',  ( 4.101954839143211906, -2.368264730583032218, -3.681130640444385982 ) ) ;
#5417=CARTESIAN_POINT ( 'NONE',  ( 2.000000000000013323, 3.464101615137772150, -3.142992957459230574 ) ) ;
#5419=EDGE_CURVE ( 'NONE', #10664, #11692, #12011, .T. ) ;
#5427=CARTESIAN_POINT ( 'NONE',  ( 2.804994570502159057, 3.229033611042447571, -3.526374918436837813 ) ) ;
#5441=EDGE_CURVE ( 'NONE', #2015, #12512, #3868, .T. ) ;
#5471=DIRECTION ( 'NONE',  ( 1.000000000000000000, 8.881784197001252323E-16, 0.000000000000000000 ) ) ;
#5477=CARTESIAN_POINT ( 'NONE',  ( 3.469446951953614189E-15, 4.618802153517009401, -0.5000000000000091038 ) ) ;
#5500=CARTESIAN_POINT ( 'NONE',  ( 4.000000000000000000, 2.309401076758511806, -0.5000000000000038858 ) ) ;
#5505=ORIENTED_EDGE ( 'NONE', *, *, #7363, .F. ) ;
#5540=ADVANCED_FACE ( 'NONE', ( #6381 ), #5667, .F. ) ;
#5541=CARTESIAN_POINT ( 'NONE',  ( -1.655952806101424146, 3.662737355149034979, -1.234974037096769500E-15 ) ) ;
#5549=CARTESIAN_POINT ( 'NONE',  ( -3.999999999999963585, -2.309401076758515359, -3.433295621305398893 ) ) ;
#5551=VECTOR ( 'NONE', #3683, 1000.000000000000000 ) ;
#5567=EDGE_LOOP ( 'NONE', ( #11623, #5831, #3703, #34, #6473, #2785, #4030 ) ) ;
#5568=ORIENTED_EDGE ( 'NONE', *, *, #7279, .T. ) ;
#5569=EDGE_CURVE ( 'NONE', #7175, #9454, #740, .T. ) ;
#5578=ADVANCED_FACE ( 'NONE', ( #7141 ), #402, .F. ) ;
#5581=CARTESIAN_POINT ( 'NONE',  ( 2.000000000000007105, 3.464101615137750390, 6.938893903907228378E-15 ) ) ;
#5587=DIRECTION ( 'NONE',  ( -1.000000000000000000, 0.000000000000000000, 0.000000000000000000 ) ) ;
#5610=DIRECTION ( 'NONE',  ( -1.000000000000000000, 0.000000000000000000, 0.000000000000000000 ) ) ;
#5632=ORIENTED_EDGE ( 'NONE', *, *, #11568, .T. ) ;
#5653=ADVANCED_FACE ( 'NONE', ( #4173, #4297 ), #6167, .T. ) ;
#5662=CARTESIAN_POINT ( 'NONE',  ( -4.203833317240843748, -1.627343821129598966, -3.597273115243905028 ) ) ;
#5667=( BOUNDED_SURFACE ( )  B_SPLINE_SURFACE ( 3, 2, ( 
 ( #11151, #389, #6251 ),
 ( #1544, #10156, #1482 ),
 ( #518, #4449, #8374 ),
 ( #1269, #8995, #7210 ),
 ( #5206, #10015, #177 ),
 ( #9123, #7016, #9889 ) ),
 .UNSPECIFIED., .F., .F., .T. ) 
 B_SPLINE_SURFACE_WITH_KNOTS ( ( 4, 2, 4 ),
 ( 3, 3 ),
 ( 0.02027065861071770947, 0.02273072267836921331, 0.02519078674602071716 ),
 ( 0.000000000000000000, 1.000000000000000000 ),
 .UNSPECIFIED. ) 
 GEOMETRIC_REPRESENTATION_ITEM ( )  RATIONAL_B_SPLINE_SURFACE ( (
 ( 1.000000000000000000, 0.8047781708337300444, 1.000000000000000000),
 ( 1.000000000000000000, 0.8123765190704228534, 1.000000000000000000),
 ( 1.000000000000000000, 0.8190656277165397903, 1.000000000000000000),
 ( 1.000000000000000000, 0.8192366903510730491, 1.000000000000000000),
 ( 1.000000000000000000, 0.8126138454303962755, 1.000000000000000000),
 ( 1.000000000000000000, 0.8047712246031432093, 1.000000000000000000) ) ) 
 REPRESENTATION_ITEM ( '' )  SURFACE ( )  );
#5674=APPLICATION_CONTEXT ( 'automotive_design' ) ;
#5678=CARTESIAN_POINT ( 'NONE',  ( -7.299729015828635442E-15, -4.736529461166059995, -3.681130640444390867 ) ) ;
#5684=ADVANCED_FACE ( 'NONE', ( #684 ), #9368, .T. ) ;
#5707=CARTESIAN_POINT ( 'NONE',  ( 0.000000000000000000, 0.000000000000000000, 0.000000000000000000 ) ) ;
#5772=EDGE_LOOP ( 'NONE', ( #2511, #5352, #4890, #8618, #7669 ) ) ;
#5782=CARTESIAN_POINT ( 'NONE',  ( 2.000000000000007105, -3.464101615137750390, -1.734723475976807094E-14 ) ) ;
#5793=EDGE_LOOP ( 'NONE', ( #6551, #9613, #413, #1124 ) ) ;
#5808=CARTESIAN_POINT ( 'NONE',  ( 2.000000000000007105, -3.464101615137750390, -1.734723475976807094E-14 ) ) ;
#5818=CARTESIAN_POINT ( 'NONE',  ( 5.560781378645591744, -2.788447640341963522E-15, -4.000000000000010658 ) ) ;
#5831=ORIENTED_EDGE ( 'NONE', *, *, #6988, .T. ) ;
#5833=CARTESIAN_POINT ( 'NONE',  ( -2.000000000000008882, -3.464101615137750390, -8.673617379884035472E-15 ) ) ;
#5835=CARTESIAN_POINT ( 'NONE',  ( 1.734723475976807094E-14, -3.469446951953614189E-15, -4.000000000000010658 ) ) ;
#5866=B_SPLINE_CURVE_WITH_KNOTS ( 'NONE', 3,
 ( #8450, #6326, #10374, #5363, #9280, #6263 ),
 .UNSPECIFIED., .F., .F.,
 ( 4, 2, 4 ),
 ( 0.000000000000000000, 0.0002095117440864779055, 0.0004190234881729558111 ),
 .UNSPECIFIED. ) ;
#5897=EDGE_LOOP ( 'NONE', ( #8733, #11176, #1079 ) ) ;
#5910=ORIENTED_EDGE ( 'NONE', *, *, #896, .F. ) ;
#5926=DIRECTION ( 'NONE',  ( 0.000000000000000000, -1.530455820933490821E-32, 1.000000000000000000 ) ) ;
#5936=AXIS2_PLACEMENT_3D ( 'NONE', #1798, #9634, #830 ) ;
#5944=FACE_OUTER_BOUND ( 'NONE', #10010, .T. ) ;
#5954=CARTESIAN_POINT ( 'NONE',  ( 5.603754474796030917E-15, 4.736522675502333080, -3.681124513963746292 ) ) ;
#5969=EDGE_CURVE ( 'NONE', #7775, #529, #11888, .T. ) ;
#5976=CARTESIAN_POINT ( 'NONE',  ( -3.453038570458820455, -2.625189405339339199, -3.535263753544679588 ) ) ;
#5981=B_SPLINE_CURVE_WITH_KNOTS ( 'NONE', 3,
 ( #774, #7737, #11664, #4119, #8758, #3109 ),
 .UNSPECIFIED., .F., .F.,
 ( 4, 2, 4 ),
 ( 0.000000000000000000, 0.0002095117440864783663, 0.0004190234881729567326 ),
 .UNSPECIFIED. ) ;
#6006=ORIENTED_EDGE ( 'NONE', *, *, #1720, .F. ) ;
#6030=AXIS2_PLACEMENT_3D ( 'NONE', #11305, #9226, #10185 ) ;
#6032=ORIENTED_EDGE ( 'NONE', *, *, #3637, .F. ) ;
#6038=CARTESIAN_POINT ( 'NONE',  ( -3.472371940585999184, -2.614027278893196193, -3.320322319202239303 ) ) ;
#6041=CARTESIAN_POINT ( 'NONE',  ( 4.000000000000000000, 0.7924765000094649015, -0.05906175389889841559 ) ) ;
#6049=ORIENTED_EDGE ( 'NONE', *, *, #3289, .F. ) ;
#6054=VECTOR ( 'NONE', #1896, 1000.000000000000227 ) ;
#6055=FACE_OUTER_BOUND ( 'NONE', #9897, .T. ) ;
#6067=ORIENTED_EDGE ( 'NONE', *, *, #8761, .F. ) ;
#6070=DIRECTION ( 'NONE',  ( -0.000000000000000000, -1.530455820933490821E-32, 1.000000000000000000 ) ) ;
#6081=EDGE_LOOP ( 'NONE', ( #9037, #6201, #2829, #7847 ) ) ;
#6092=CARTESIAN_POINT ( 'NONE',  ( 4.000000000000000000, 2.309401076758487381, -4.999999999999984013 ) ) ;
#6099=ORIENTED_EDGE ( 'NONE', *, *, #4308, .T. ) ;
#6104=CARTESIAN_POINT ( 'NONE',  ( -3.540020015735288350, -2.810662092923964739, -3.602146406945708090 ) ) ;
#6105=ADVANCED_FACE ( 'NONE', ( #7173 ), #818, .F. ) ;
#6109=CARTESIAN_POINT ( 'NONE',  ( -2.171643655288376884, 3.365003104552322544, -1.490401528079900172E-15 ) ) ;
#6122=CARTESIAN_POINT ( 'NONE',  ( -3.999999999999991562, 1.941961291383474952, -0.3515519931180154933 ) ) ;
#6136=CARTESIAN_POINT ( 'NONE',  ( -3.999999999999993339, -0.8382240730042115340, -3.220610619767148020 ) ) ;
#6145=MECHANICAL_DESIGN_GEOMETRIC_PRESENTATION_REPRESENTATION('',(#9631),#4096);
#6161=B_SPLINE_CURVE_WITH_KNOTS ( 'NONE', 3,
 ( #2934, #9783, #4782, #5678, #8712, #6783 ),
 .UNSPECIFIED., .F., .F.,
 ( 4, 2, 4 ),
 ( 0.000000000000000000, 0.0002095117440864791795, 0.0004190234881729583589 ),
 .UNSPECIFIED. ) ;
#6167=PLANE ( 'NONE',  #5071 ) ;
#6184=SURFACE_SIDE_STYLE ('',( #2264 ) ) ;
#6188=CARTESIAN_POINT ( 'NONE',  ( -0.6666666666666353214, -4.233901974057276973, -3.300726591567087809 ) ) ;
#6192=CARTESIAN_POINT ( 'NONE',  ( 4.140404888673280048, 2.228338276487438208, -3.686887068327037831 ) ) ;
#6201=ORIENTED_EDGE ( 'NONE', *, *, #10417, .T. ) ;
#6207=VECTOR ( 'NONE', #6974, 1000.000000000000114 ) ;
#6229=DIRECTION ( 'NONE',  ( -1.000000000000000000, 0.000000000000000000, 0.000000000000000000 ) ) ;
#6231=CARTESIAN_POINT ( 'NONE',  ( -2.742827927723363590, -3.035229711104975081, -3.433252694550608553 ) ) ;
#6238=CARTESIAN_POINT ( 'NONE',  ( 3.522875095019549985, -2.820352903225599395, -3.598441714920586953 ) ) ;
#6248=FACE_OUTER_BOUND ( 'NONE', #1862, .T. ) ;
#6251=CARTESIAN_POINT ( 'NONE',  ( 4.211399257449711442, -2.459727064652543316, -3.751161691472425730 ) ) ;
#6262=CARTESIAN_POINT ( 'NONE',  ( -4.197312064133464915, -0.8182229787990212833, -3.502518405183899564 ) ) ;
#6263=CARTESIAN_POINT ( 'NONE',  ( 4.211140560182228043, -2.431303136016558231, -3.745885042887437510 ) ) ;
#6271=CARTESIAN_POINT ( 'NONE',  ( -4.024497503033714452, 2.323544716729490478, -3.572167766733773675 ) ) ;
#6278=EDGE_CURVE ( 'NONE', #5156, #10905, #10798, .T. ) ;
#6279=CARTESIAN_POINT ( 'NONE',  ( -4.000000000000012434, 2.309401076758501592, -3.433295621305395340 ) ) ;
#6285=CARTESIAN_POINT ( 'NONE',  ( -4.141042297810622053, 2.227970268150405886, -3.687027686973636253 ) ) ;
#6295=ORIENTED_EDGE ( 'NONE', *, *, #5262, .F. ) ;
#6299=CARTESIAN_POINT ( 'NONE',  ( -3.861362476283222378, -2.629030857716012637, -3.671615880910391372 ) ) ;
#6300=CARTESIAN_POINT ( 'NONE',  ( 0.000000000000000000, 0.000000000000000000, 0.000000000000000000 ) ) ;
#6326=CARTESIAN_POINT ( 'NONE',  ( 4.000000000000022204, -2.309401076758519800, -3.504271511727111044 ) ) ;
#6332=ORIENTED_EDGE ( 'NONE', *, *, #4360, .F. ) ;
#6333=CARTESIAN_POINT ( 'NONE',  ( -4.000000000000015099, 2.309401076758498927, -3.504269196027880895 ) ) ;
#6346=AXIS2_PLACEMENT_3D ( 'NONE', #3538, #6558, #7712 ) ;
#6351=ORIENTED_EDGE ( 'NONE', *, *, #12089, .T. ) ;
#6361=CONICAL_SURFACE ( 'NONE', #9221, 5.560781378645573980, 1.221730476396046816 ) ;
#6381=FACE_OUTER_BOUND ( 'NONE', #166, .T. ) ;
#6385=CARTESIAN_POINT ( 'NONE',  ( 2.742827927723509696, 3.035229711105237538, -3.433252694550597450 ) ) ;
#6403=CARTESIAN_POINT ( 'NONE',  ( -4.000000000000012434, 2.309401076758501592, -3.433295621305395340 ) ) ;
#6407=B_SPLINE_CURVE_WITH_KNOTS ( 'NONE', 3,
 ( #1950, #4667, #9665, #12660, #1700 ),
 .UNSPECIFIED., .F., .F.,
 ( 4, 1, 4 ),
 ( 0.000000000000000000, 0.002309401076758506224, 0.004618802153517012447 ),
 .UNSPECIFIED. ) ;
#6428=DIRECTION ( 'NONE',  ( 1.000000000000000000, 0.000000000000000000, 0.000000000000000000 ) ) ;
#6446=AXIS2_PLACEMENT_3D ( 'NONE', #4971, #9713, #9780 ) ;
#6458=CARTESIAN_POINT ( 'NONE',  ( 4.000000000000002665, 1.539600717838986110, -3.300726591567064716 ) ) ;
#6466=B_SPLINE_CURVE_WITH_KNOTS ( 'NONE', 3,
 ( #182, #373, #4112, #3357, #7276, #11199, #6299, #10208 ),
 .UNSPECIFIED., .F., .F.,
 ( 4, 2, 2, 4 ),
 ( 0.000000000000000000, 0.002450665683189819262, 0.003675998524784728893, 0.004901331366379638524 ),
 .UNSPECIFIED. ) ;
#6473=ORIENTED_EDGE ( 'NONE', *, *, #8108, .T. ) ;
#6488=AXIS2_PLACEMENT_3D ( 'NONE', #3894, #9796, #11689 ) ;
#6497=FACE_OUTER_BOUND ( 'NONE', #5897, .T. ) ;
#6504=UNCERTAINTY_MEASURE_WITH_UNIT (LENGTH_MEASURE( 1.000000000000000082E-05 ), #3934, 'distance_accuracy_value', 'NONE');
#6527=ORIENTED_EDGE ( 'NONE', *, *, #5419, .T. ) ;
#6551=ORIENTED_EDGE ( 'NONE', *, *, #3563, .F. ) ;
#6558=DIRECTION ( 'NONE',  ( 0.000000000000000000, 1.530455820933490821E-32, -1.000000000000000000 ) ) ;
#6561=CARTESIAN_POINT ( 'NONE',  ( 0.3208286057739622166, -4.433571671609698228, -0.3503314178412686997 ) ) ;
#6562=ADVANCED_FACE ( 'NONE', ( #2513 ), #4209, .T. ) ;
#6579=EDGE_CURVE ( 'NONE', #38, #4694, #2357, .T. ) ;
#6585=CARTESIAN_POINT ( 'NONE',  ( -0.02511973781849641263, 4.877415612947407553, -3.751298745799847456 ) ) ;
#6587=CARTESIAN_POINT ( 'NONE',  ( -4.101948962586043024, -2.368261337751181639, -3.681124513963744516 ) ) ;
#6620=ORIENTED_EDGE ( 'NONE', *, *, #10728, .F. ) ;
#6629=AXIS2_PLACEMENT_3D ( 'NONE', #4152, #157, #9930 ) ;
#6745=CIRCLE ( 'NONE', #1381, 2.500000000000000444 ) ;
#6751=DIRECTION ( 'NONE',  ( 1.000000000000000000, 0.000000000000000000, 0.000000000000000000 ) ) ;
#6778=AXIS2_PLACEMENT_3D ( 'NONE', #2681, #4602, #11680 ) ;
#6783=CARTESIAN_POINT ( 'NONE',  ( 3.122502256758252770E-14, -4.862606272033112909, -3.745885042887444616 ) ) ;
#6794=ORIENTED_EDGE ( 'NONE', *, *, #8131, .T. ) ;
#6811=EDGE_LOOP ( 'NONE', ( #8139, #1065, #6295, #9674 ) ) ;
#6825=EDGE_LOOP ( 'NONE', ( #497, #6332 ) ) ;
#6835=CARTESIAN_POINT ( 'NONE',  ( 1.257172072275555497, -3.892973519170928043, -3.433252694550785300 ) ) ;
#6836=VECTOR ( 'NONE', #9018, 999.9999999999998863 ) ;
#6843=EDGE_CURVE ( 'NONE', #927, #3906, #7095, .T. ) ;
#6865=FACE_OUTER_BOUND ( 'NONE', #417, .T. ) ;
#6882=DIRECTION ( 'NONE',  ( -1.000000000000000000, 0.000000000000000000, 0.000000000000000000 ) ) ;
#6896=CARTESIAN_POINT ( 'NONE',  ( -0.1750025118121416035, -4.719839900820628209, -3.469254087858258284 ) ) ;
#6934=CARTESIAN_POINT ( 'NONE',  ( 0.000000000000000000, 4.862606272033057841, -3.745885042887454830 ) ) ;
#6938=ORIENTED_EDGE ( 'NONE', *, *, #6579, .T. ) ;
#6952=CARTESIAN_POINT ( 'NONE',  ( 0.000000000000000000, 4.618802153517012954, -5.000000000000018652 ) ) ;
#6957=CARTESIAN_POINT ( 'NONE',  ( 4.000000000000000000, -2.309401076758522464, -5.000000000000000888 ) ) ;
#6969=CARTESIAN_POINT ( 'NONE',  ( -3.999999999999994671, -2.309401076758511806, -0.4999999999999865663 ) ) ;
#6974=DIRECTION ( 'NONE',  ( -0.8191520442889902442, 8.778333957637496424E-33, -0.5735764363510482688 ) ) ;
#6978=ORIENTED_EDGE ( 'NONE', *, *, #3848, .T. ) ;
#6988=EDGE_CURVE ( 'NONE', #7688, #222, #11748, .T. ) ;
#6993=CARTESIAN_POINT ( 'NONE',  ( 0.000000000000000000, 4.618802153516985420, -3.433295621305398893 ) ) ;
#6995=ORIENTED_EDGE ( 'NONE', *, *, #4239, .T. ) ;
#7002=FACE_OUTER_BOUND ( 'NONE', #370, .T. ) ;
#7006=LINE ( 'NONE', #9114, #10635 ) ;
#7016=CARTESIAN_POINT ( 'NONE',  ( 4.000000000000001776, 2.472263674411383505, -3.687027874309860564 ) ) ;
#7022=ADVANCED_FACE ( 'NONE', ( #9172 ), #10162, .F. ) ;
#7044=CARTESIAN_POINT ( 'NONE',  ( -2.500000000000000444, -3.438830781974930402E-14, -25.03750572909320837 ) ) ;
#7048=EDGE_LOOP ( 'NONE', ( #173, #98, #10369, #8397 ) ) ;
#7078=CARTESIAN_POINT ( 'NONE',  ( -4.140404888673263173, -2.228338276487473291, -3.686887068327048045 ) ) ;
#7079=ORIENTED_EDGE ( 'NONE', *, *, #1228, .T. ) ;
#7081=CARTESIAN_POINT ( 'NONE',  ( 5.384454397937153303, -3.469446951953614189E-15, -4.484454397937126302 ) ) ;
#7085=DIRECTION ( 'NONE',  ( -1.000000000000000000, 0.000000000000000000, 0.000000000000000000 ) ) ;
#7095=CIRCLE ( 'NONE', #10591, 4.000000000000000000 ) ;
#7103=DIRECTION ( 'NONE',  ( 0.000000000000000000, -1.530455820933490821E-32, 1.000000000000000000 ) ) ;
#7111=CARTESIAN_POINT ( 'NONE',  ( -3.999999999999993339, 2.471528634177572847, -3.686887442155197370 ) ) ;
#7131=CARTESIAN_POINT ( 'NONE',  ( -3.999999999999994671, 0.000000000000000000, 8.673617379884035472E-15 ) ) ;
#7134=CARTESIAN_POINT ( 'NONE',  ( -2.807080416178834525, 3.225969019225355616, -3.502507215260556528 ) ) ;
#7141=FACE_OUTER_BOUND ( 'NONE', #6811, .T. ) ;
#7144=CARTESIAN_POINT ( 'NONE',  ( 4.000000000000000000, 0.1981133338132478328, 8.576208590949790933E-18 ) ) ;
#7154=ADVANCED_FACE ( 'NONE', ( #11629 ), #8466, .F. ) ;
#7165=CARTESIAN_POINT ( 'NONE',  ( 4.000000000000000000, -2.309401076758518911, -0.4999999999999917843 ) ) ;
#7167=CARTESIAN_POINT ( 'NONE',  ( 2.756197834950067982, 3.027510591568718823, -3.223146290109625944 ) ) ;
#7173=FACE_OUTER_BOUND ( 'NONE', #3151, .T. ) ;
#7175=VERTEX_POINT ( 'NONE', #8786 ) ;
#7189=ORIENTED_EDGE ( 'NONE', *, *, #8131, .F. ) ;
#7196=ADVANCED_FACE ( 'NONE', ( #6865 ), #11013, .F. ) ;
#7209=PRODUCT ( 'hex flange nut gradea_iso_ISO - 4161 - M5 - N', 'hex flange nut gradea_iso_ISO - 4161 - M5 - N', '', ( #10976 ) ) ;
#7210=CARTESIAN_POINT ( 'NONE',  ( 4.197310751797295403, 0.8178363989516003185, -3.502498386812445741 ) ) ;
#7219=DIRECTION ( 'NONE',  ( 0.000000000000000000, 1.530455820933490821E-32, -1.000000000000000000 ) ) ;
#7230=EDGE_CURVE ( 'NONE', #962, #7688, #12380, .T. ) ;
#7248=DIRECTION ( 'NONE',  ( 1.000000000000000000, 0.000000000000000000, 0.000000000000000000 ) ) ;
#7262=ORIENTED_EDGE ( 'NONE', *, *, #2270, .T. ) ;
#7263=CARTESIAN_POINT ( 'NONE',  ( -3.522875095019470937, 2.820352903225139762, -3.598441714920489698 ) ) ;
#7266=ORIENTED_EDGE ( 'NONE', *, *, #2811, .T. ) ;
#7276=CARTESIAN_POINT ( 'NONE',  ( -2.804994570502143070, -3.229033611042466223, -3.526374918436845807 ) ) ;
#7279=EDGE_CURVE ( 'NONE', #3906, #10905, #11434, .T. ) ;
#7282=ORIENTED_EDGE ( 'NONE', *, *, #7748, .F. ) ;
#7289=AXIS2_PLACEMENT_3D ( 'NONE', #3693, #718, #7969 ) ;
#7300=CARTESIAN_POINT ( 'NONE',  ( -4.211140560182210280, 2.431303136016527144, -3.745885042887430405 ) ) ;
#7303=CARTESIAN_POINT ( 'NONE',  ( -3.999999999999993339, 0.8730739991738295513, -3.223134629628441328 ) ) ;
#7310=DIRECTION ( 'NONE',  ( 0.000000000000000000, -1.530455820933490821E-32, 1.000000000000000000 ) ) ;
#7334=ORIENTED_EDGE ( 'NONE', *, *, #2616, .F. ) ;
#7358=B_SPLINE_CURVE_WITH_KNOTS ( 'NONE', 3,
 ( #9324, #5541, #4447, #3490, #1543, #5477 ),
 .UNSPECIFIED., .F., .F.,
 ( 4, 2, 4 ),
 ( 0.002365888236227973833, 0.003551327329835075874, 0.004736766423442177916 ),
 .UNSPECIFIED. ) ;
#7363=EDGE_CURVE ( 'NONE', #10248, #4329, #1147, .T. ) ;
#7364=ORIENTED_EDGE ( 'NONE', *, *, #2345, .T. ) ;
#7392=DIRECTION ( 'NONE',  ( 0.000000000000000000, 0.000000000000000000, 1.000000000000000000 ) ) ;
#7402=CARTESIAN_POINT ( 'NONE',  ( 0.000000000000000000, 0.000000000000000000, 0.000000000000000000 ) ) ;
#7403=AXIS2_PLACEMENT_3D ( 'NONE', #4897, #3929, #9641 ) ;
#7422=CARTESIAN_POINT ( 'NONE',  ( 0.6666666666666680729, 4.233901974057235229, -3.300726591567098023 ) ) ;
#7465=CONICAL_SURFACE ( 'NONE', #3564, 2.500000000000000888, 0.9599310885968785900 ) ;
#7467=CARTESIAN_POINT ( 'NONE',  ( 0.000000000000000000, 0.000000000000000000, -0.2800830152838839626 ) ) ;
#7481=FACE_OUTER_BOUND ( 'NONE', #5793, .T. ) ;
#7483=CIRCLE ( 'NONE', #7289, 2.499999999999999556 ) ;
#7523=CARTESIAN_POINT ( 'NONE',  ( 2.000000000000007105, -3.464101615137750390, -1.734723475976807094E-14 ) ) ;
#7562=CARTESIAN_POINT ( 'NONE',  ( -2.099999999999965450, -3.212271124132670141E-15, -4.694516984716123886 ) ) ;
#7606=EDGE_LOOP ( 'NONE', ( #4541, #7858, #8807, #7282 ) ) ;
#7621=DIRECTION ( 'NONE',  ( 0.000000000000000000, -1.530455820933490821E-32, 1.000000000000000000 ) ) ;
#7635=ORIENTED_EDGE ( 'NONE', *, *, #10367, .T. ) ;
#7657=EDGE_LOOP ( 'NONE', ( #10075, #10263, #6351, #9047, #7364 ) ) ;
#7663=CARTESIAN_POINT ( 'NONE',  ( 3.680118525130243956, -2.494084732383345493, -0.3507732604232523532 ) ) ;
#7667=CARTESIAN_POINT ( 'NONE',  ( -4.197393957002295117, -8.025123413315649349E-14, -3.503767560748944021 ) ) ;
#7668=CARTESIAN_POINT ( 'NONE',  ( 0.000000000000000000, 4.618802153517012954, -5.000000000000018652 ) ) ;
#7669=ORIENTED_EDGE ( 'NONE', *, *, #5969, .F. ) ;
#7688=VERTEX_POINT ( 'NONE', #9784 ) ;
#7689=EDGE_CURVE ( 'NONE', #10242, #10664, #2375, .T. ) ;
#7693=CARTESIAN_POINT ( 'NONE',  ( 4.000000000000000000, -1.560351142792954171, -0.2242961665059817755 ) ) ;
#7698=DIRECTION ( 'NONE',  ( 0.000000000000000000, -1.530455820933490821E-32, 1.000000000000000000 ) ) ;
#7710=ORIENTED_EDGE ( 'NONE', *, *, #6579, .F. ) ;
#7712=DIRECTION ( 'NONE',  ( -1.000000000000000000, 0.000000000000000000, 0.000000000000000000 ) ) ;
#7726=ORIENTED_EDGE ( 'NONE', *, *, #11568, .F. ) ;
#7732=EDGE_CURVE ( 'NONE', #11692, #927, #1964, .T. ) ;
#7733=CARTESIAN_POINT ( 'NONE',  ( 0.5276280594148604619, -4.314175951381856500, -3.320322319202345440 ) ) ;
#7737=CARTESIAN_POINT ( 'NONE',  ( 4.000000000000002665, 2.309401076758486937, -3.504271511727107047 ) ) ;
#7741=CIRCLE ( 'NONE', #8380, 5.384454397937118664 ) ;
#7748=EDGE_CURVE ( 'NONE', #10993, #11393, #1938, .T. ) ;
#7775=VERTEX_POINT ( 'NONE', #7165 ) ;
#7807=CARTESIAN_POINT ( 'NONE',  ( 3.122502256758252770E-14, -4.862606272033112909, -3.745885042887444616 ) ) ;
#7813=ORIENTED_EDGE ( 'NONE', *, *, #6843, .F. ) ;
#7828=ORIENTED_EDGE ( 'NONE', *, *, #8344, .T. ) ;
#7833=DIRECTION ( 'NONE',  ( 0.000000000000000000, -1.530455820933490821E-32, 1.000000000000000000 ) ) ;
#7847=ORIENTED_EDGE ( 'NONE', *, *, #8344, .F. ) ;
#7852=FACE_OUTER_BOUND ( 'NONE', #7048, .T. ) ;
#7858=ORIENTED_EDGE ( 'NONE', *, *, #3637, .T. ) ;
#7859=CARTESIAN_POINT ( 'NONE',  ( -3.999999999999970690, -2.309401076758515359, -5.000000000000018652 ) ) ;
#7865=CARTESIAN_POINT ( 'NONE',  ( -3.999999999999991562, -1.560351142792946622, -0.2242961665059734766 ) ) ;
#7879=CARTESIAN_POINT ( 'NONE',  ( 4.000000000000001776, 2.309401076758487381, -3.433295621305364254 ) ) ;
#7901=CARTESIAN_POINT ( 'NONE',  ( 3.122502256758252770E-14, -4.618802153517027165, -3.433295621305388678 ) ) ;
#7909=FACE_OUTER_BOUND ( 'NONE', #1040, .T. ) ;
#7926=DIRECTION ( 'NONE',  ( -1.000000000000000000, 0.000000000000000000, 0.000000000000000000 ) ) ;
#7937=DIRECTION ( 'NONE',  ( 0.000000000000000000, 1.530455820933490821E-32, -1.000000000000000000 ) ) ;
#7945=CARTESIAN_POINT ( 'NONE',  ( 1.925929944387235853E-31, 4.618802153516985420, -3.504269196027888444 ) ) ;
#7969=DIRECTION ( 'NONE',  ( 1.000000000000000000, 0.000000000000000000, 0.000000000000000000 ) ) ;
#7981=ADVANCED_FACE ( 'NONE', ( #3623 ), #10553, .F. ) ;
#7993=CARTESIAN_POINT ( 'NONE',  ( -3.999999999999993339, 1.700094919196852850, -3.320312364301083008 ) ) ;
#7996=CARTESIAN_POINT ( 'NONE',  ( 0.000000000000000000, 0.000000000000000000, -0.3080913168122742518 ) ) ;
#8009=CARTESIAN_POINT ( 'NONE',  ( -1.999999999999997335, 3.464101615137737067, -3.142992957459241676 ) ) ;
#8018=CARTESIAN_POINT ( 'NONE',  ( -2.775557561562891351E-14, -4.618802153517012954, -0.5000000000000004441 ) ) ;
#8027=EDGE_LOOP ( 'NONE', ( #10789, #6099 ) ) ;
#8030=CARTESIAN_POINT ( 'NONE',  ( -4.175002511812136774, -2.208363329454923196, -3.469254087858258728 ) ) ;
#8033=STYLED_ITEM ( 'NONE', ( #384 ), #10947 ) ;
#8036=CARTESIAN_POINT ( 'NONE',  ( 0.000000000000000000, 0.000000000000000000, 0.000000000000000000 ) ) ;
#8047=CARTESIAN_POINT ( 'NONE',  ( -2.682243648011668480, -3.070208061305304437, -0.04852650426601311934 ) ) ;
#8085=CARTESIAN_POINT ( 'NONE',  ( 0.1750025118121487089, 4.719839900820611334, -3.469254087858254731 ) ) ;
#8088=EDGE_LOOP ( 'NONE', ( #3228, #9164, #7334 ) ) ;
#8106=AXIS2_PLACEMENT_3D ( 'NONE', #973, #8888, #2071 ) ;
#8108=EDGE_CURVE ( 'NONE', #8996, #11904, #11020, .T. ) ;
#8109=DIRECTION ( 'NONE',  ( 0.5000000000000022204, 0.8660254037844374864, 0.000000000000000000 ) ) ;
#8115=CIRCLE ( 'NONE', #8535, 4.000000000000000000 ) ;
#8121=ORIENTED_EDGE ( 'NONE', *, *, #8761, .T. ) ;
#8131=EDGE_CURVE ( 'NONE', #529, #10905, #8115, .T. ) ;
#8139=ORIENTED_EDGE ( 'NONE', *, *, #11842, .F. ) ;
#8161=ADVANCED_FACE ( 'NONE', ( #7852 ), #3129, .F. ) ;
#8162=CARTESIAN_POINT ( 'NONE',  ( -2.756197834950048442, -3.027510591568753462, -3.223146290110009193 ) ) ;
#8173=B_SPLINE_CURVE_WITH_KNOTS ( 'NONE', 3,
 ( #1496, #655, #4597, #10174, #5427, #9341, #4465, #2414 ),
 .UNSPECIFIED., .F., .F.,
 ( 4, 2, 2, 4 ),
 ( 0.000000000000000000, 0.002450665683189816660, 0.003675998524784724990, 0.004901331366379633320 ),
 .UNSPECIFIED. ) ;
#8179=AXIS2_PLACEMENT_3D ( 'NONE', #3667, #3729, #11396 ) ;
#8193=CARTESIAN_POINT ( 'NONE',  ( -4.197477534772225738, 0.8522413273724327443, -3.505042416683237683 ) ) ;
#8200=ORIENTED_EDGE ( 'NONE', *, *, #11234, .T. ) ;
#8211=CONICAL_SURFACE ( 'NONE', #2682, 5.560781378645573980, 1.221730476396046816 ) ;
#8217=CARTESIAN_POINT ( 'NONE',  ( -2.712762565639325718, 3.052587955997613456, -3.430618716626822717 ) ) ;
#8227=CARTESIAN_POINT ( 'NONE',  ( 3.469446951953614189E-14, -3.469446951953614189E-15, -4.974600000000009459 ) ) ;
#8230=DIRECTION ( 'NONE',  ( -1.000000000000000000, 0.000000000000000000, 0.000000000000000000 ) ) ;
#8241=ORIENTED_EDGE ( 'NONE', *, *, #10237, .T. ) ;
#8245=FILL_AREA_STYLE_COLOUR ( '', #10700 ) ;
#8251=EDGE_CURVE ( 'NONE', #10664, #927, #12457, .T. ) ;
#8258=ORIENTED_EDGE ( 'NONE', *, *, #345, .T. ) ;
#8280=CARTESIAN_POINT ( 'NONE',  ( -1.257172072275692054, 3.892973519170934260, -3.433252694550601447 ) ) ;
#8294=DIRECTION ( 'NONE',  ( 1.000000000000000000, 0.000000000000000000, 0.000000000000000000 ) ) ;
#8302=CIRCLE ( 'NONE', #2779, 2.100000000000000089 ) ;
#8306=( NAMED_UNIT ( * ) PLANE_ANGLE_UNIT ( ) SI_UNIT ( $, .RADIAN. ) );
#8307=CARTESIAN_POINT ( 'NONE',  ( 4.000000000000000000, 2.309401076758487381, -4.999999999999984013 ) ) ;
#8324=DIRECTION ( 'NONE',  ( 0.000000000000000000, -1.530455820933490821E-32, 1.000000000000000000 ) ) ;
#8344=EDGE_CURVE ( 'NONE', #2170, #12673, #1533, .T. ) ;
#8345=AXIS2_PLACEMENT_3D ( 'NONE', #1113, #7937, #4801 ) ;
#8360=FACE_OUTER_BOUND ( 'NONE', #9539, .T. ) ;
#8374=CARTESIAN_POINT ( 'NONE',  ( 4.197478902586993854, -0.8524102783748621626, -3.505063281295508038 ) ) ;
#8380=AXIS2_PLACEMENT_3D ( 'NONE', #880, #9879, #6751 ) ;
#8396=ADVANCED_FACE ( 'NONE', ( #8360 ), #5044, .T. ) ;
#8397=ORIENTED_EDGE ( 'NONE', *, *, #3515, .F. ) ;
#8420=COLOUR_RGB ( '', 0.09019608, 0.27058824, 0.51372549) ;
#8450=CARTESIAN_POINT ( 'NONE',  ( 4.000000000000019540, -2.309401076758522464, -3.433295621305367806 ) ) ;
#8455=CARTESIAN_POINT ( 'NONE',  ( -5.560781378645554440, -2.788447640341961550E-15, -4.000000000000010658 ) ) ;
#8466=PLANE ( 'NONE',  #4010 ) ;
#8518=CARTESIAN_POINT ( 'NONE',  ( -3.999999999999963585, -2.309401076758515359, -3.433295621305398893 ) ) ;
#8519=ORIENTED_EDGE ( 'NONE', *, *, #7230, .F. ) ;
#8535=AXIS2_PLACEMENT_3D ( 'NONE', #770, #4702, #10678 ) ;
#8568=EDGE_CURVE ( 'NONE', #11904, #10248, #91, .T. ) ;
#8574=AXIS2_PLACEMENT_3D ( 'NONE', #214, #5051, #2287 ) ;
#8586=VERTEX_POINT ( 'NONE', #7879 ) ;
#8594=CARTESIAN_POINT ( 'NONE',  ( 4.000000000000000000, 2.309401076758487381, -4.999999999999984013 ) ) ;
#8607=CARTESIAN_POINT ( 'NONE',  ( 0.000000000000000000, 0.000000000000000000, 0.000000000000000000 ) ) ;
#8618=ORIENTED_EDGE ( 'NONE', *, *, #2758, .F. ) ;
#8628=CARTESIAN_POINT ( 'NONE',  ( 1.243802165048784492, -3.900692638707469850, -3.223146290109814682 ) ) ;
#8651=CARTESIAN_POINT ( 'NONE',  ( 2.344047193898584958, 3.265465875126461803, 6.475990398232750876E-15 ) ) ;
#8673=VERTEX_POINT ( 'NONE', #4272 ) ;
#8693=ADVANCED_FACE ( 'NONE', ( #2223 ), #4411, .T. ) ;
#8696=LINE ( 'NONE', #6957, #9028 ) ;
#8712=CARTESIAN_POINT ( 'NONE',  ( -2.927912186991283461E-13, -4.796980096169334296, -3.721999068284310930 ) ) ;
#8733=ORIENTED_EDGE ( 'NONE', *, *, #8251, .T. ) ;
#8758=CARTESIAN_POINT ( 'NONE',  ( 4.154306624730862652, 2.398490048084779502, -3.721999068284283396 ) ) ;
#8761=EDGE_CURVE ( 'NONE', #1828, #5156, #3636, .T. ) ;
#8786=CARTESIAN_POINT ( 'NONE',  ( -2.499999999999999556, 3.061616997868382648E-16, 3.469446951953614189E-15 ) ) ;
#8792=EDGE_LOOP ( 'NONE', ( #7635, #12537, #2719, #11955 ) ) ;
#8794=EDGE_CURVE ( 'NONE', #10905, #9298, #3354, .T. ) ;
#8807=ORIENTED_EDGE ( 'NONE', *, *, #11639, .T. ) ;
#8811=AXIS2_PLACEMENT_3D ( 'NONE', #8607, #4687, #5587 ) ;
#8815=DIRECTION ( 'NONE',  ( -0.8660254037844377084, -0.5000000000000015543, 1.972152263052529295E-31 ) ) ;
#8818=PLANE ( 'NONE',  #2909 ) ;
#8828=CARTESIAN_POINT ( 'NONE',  ( -3.999999999999990674, -0.7890432684750864345, -0.04868663549881568908 ) ) ;
#8839=DIRECTION ( 'NONE',  ( 0.9396926207859138680, 1.150791560227856926E-16, -0.3420201433256536139 ) ) ;
#8858=SURFACE_SIDE_STYLE ('',( #10915 ) ) ;
#8873=CONICAL_SURFACE ( 'NONE', #9273, 4.000000000000000000, 0.8911886515913786111 ) ;
#8888=DIRECTION ( 'NONE',  ( 0.000000000000000000, 1.530455820933490821E-32, -1.000000000000000000 ) ) ;
#8918=ORIENTED_EDGE ( 'NONE', *, *, #8108, .F. ) ;
#8919=( LENGTH_UNIT ( ) NAMED_UNIT ( * ) SI_UNIT ( .MILLI., .METRE. ) );
#8942=DIRECTION ( 'NONE',  ( 0.000000000000000000, 1.530455820933490821E-32, -1.000000000000000000 ) ) ;
#8951=CARTESIAN_POINT ( 'NONE',  ( -0.6937372685066772737, 4.453844082567717244, -3.610536846335900218 ) ) ;
#8966=ORIENTED_EDGE ( 'NONE', *, *, #11169, .T. ) ;
#8974=CARTESIAN_POINT ( 'NONE',  ( 0.000000000000000000, 4.618802153516985420, -3.433295621305398893 ) ) ;
#8988=B_SPLINE_CURVE_WITH_KNOTS ( 'NONE', 3,
 ( #6934, #4023, #5954, #1055, #7945, #6993 ),
 .UNSPECIFIED., .F., .F.,
 ( 4, 2, 4 ),
 ( -3.640115492411093008E-06, 0.0002066546034003419164, 0.0004169493222930948902 ),
 .UNSPECIFIED. ) ;
#8995=CARTESIAN_POINT ( 'NONE',  ( 4.000000000000001776, 0.8228435280417438769, -3.430609588141305899 ) ) ;
#8996=VERTEX_POINT ( 'NONE', #3120 ) ;
#8997=CARTESIAN_POINT ( 'NONE',  ( 4.000000000000000000, 0.3987449864460003712, -0.01220643443059823453 ) ) ;
#9002=PRODUCT_DEFINITION ( 'UNKNOWN', '', #12504, #4439 ) ;
#9017=B_SPLINE_CURVE_WITH_KNOTS ( 'NONE', 3,
 ( #449, #10095, #3246, #9262, #3371, #12186, #6122, #4380 ),
 .UNSPECIFIED., .F., .F.,
 ( 4, 2, 2, 4 ),
 ( 0.005725059856848637406, 0.006314084072593623143, 0.006903108288338608012, 0.008081156719828579485 ),
 .UNSPECIFIED. ) ;
#9018=DIRECTION ( 'NONE',  ( -0.8191520442889875797, 1.003171929053519447E-16, 0.5735764363510522656 ) ) ;
#9028=VECTOR ( 'NONE', #1086, 1000.000000000000000 ) ;
#9037=ORIENTED_EDGE ( 'NONE', *, *, #10367, .F. ) ;
#9047=ORIENTED_EDGE ( 'NONE', *, *, #7732, .T. ) ;
#9060=DIRECTION ( 'NONE',  ( 1.000000000000000000, 0.000000000000000000, 0.000000000000000000 ) ) ;
#9061=ORIENTED_EDGE ( 'NONE', *, *, #9481, .T. ) ;
#9082=CARTESIAN_POINT ( 'NONE',  ( 2.500000000000035527, -3.469446951953657734E-14, -5.000000000000011546 ) ) ;
#9101=ORIENTED_EDGE ( 'NONE', *, *, #11543, .F. ) ;
#9103=VERTEX_POINT ( 'NONE', #9082 ) ;
#9114=CARTESIAN_POINT ( 'NONE',  ( -3.999999999999991562, 2.309401076758501592, -4.999999999999993783 ) ) ;
#9118=ORIENTED_EDGE ( 'NONE', *, *, #7279, .F. ) ;
#9123=CARTESIAN_POINT ( 'NONE',  ( 4.000000000000001776, 2.512223110932509940, -3.469391141908801934 ) ) ;
#9139=DIRECTION ( 'NONE',  ( 0.000000000000000000, 1.530455820933490821E-32, -1.000000000000000000 ) ) ;
#9164=ORIENTED_EDGE ( 'NONE', *, *, #11877, .T. ) ;
#9172=FACE_OUTER_BOUND ( 'NONE', #11813, .T. ) ;
#9199=SHAPE_REPRESENTATION ( 'hex flange nut gradea_iso_ISO - 4161 - M5 - N', ( #12422 ), #10082 ) ;
#9214=CARTESIAN_POINT ( 'NONE',  ( -3.999999999999993339, -2.512220745329314830, -3.469390707569731447 ) ) ;
#9215=CARTESIAN_POINT ( 'NONE',  ( 3.469446951953614189E-15, 4.618802153517009401, -0.5000000000000091038 ) ) ;
#9221=AXIS2_PLACEMENT_3D ( 'NONE', #5835, #9748, #941 ) ;
#9226=DIRECTION ( 'NONE',  ( -0.000000000000000000, 1.530455820933490821E-32, -1.000000000000000000 ) ) ;
#9262=CARTESIAN_POINT ( 'NONE',  ( -3.999999999999990674, 0.7924765000094612377, -0.05906175389889126159 ) ) ;
#9271=CARTESIAN_POINT ( 'NONE',  ( 0.000000000000000000, 4.618802153516985420, -3.433295621305398893 ) ) ;
#9273=AXIS2_PLACEMENT_3D ( 'NONE', #4058, #9139, #12122 ) ;
#9274=ADVANCED_FACE ( 'NONE', ( #1548 ), #8211, .T. ) ;
#9280=CARTESIAN_POINT ( 'NONE',  ( 4.154306624730794262, -2.398490048084974013, -3.721999068284304713 ) ) ;
#9290=CARTESIAN_POINT ( 'NONE',  ( -5.384454397937084025, -2.810041467594755935E-15, -4.484454397937126302 ) ) ;
#9296=CARTESIAN_POINT ( 'NONE',  ( 4.207491450040597769, -2.029819825146486956, -3.671670828759570515 ) ) ;
#9298=VERTEX_POINT ( 'NONE', #3495 ) ;
#9300=CIRCLE ( 'NONE', #6446, 2.500000000000000444 ) ;
#9311=CIRCLE ( 'NONE', #11797, 0.5155456020628804703 ) ;
#9321=SURFACE_STYLE_USAGE ( .BOTH. , #6184 ) ;
#9324=CARTESIAN_POINT ( 'NONE',  ( -2.000000000000005329, 3.464101615137750390, 1.561251128379126385E-14 ) ) ;
#9330=CARTESIAN_POINT ( 'NONE',  ( 3.453038570460582157, 2.625189405341364690, -3.535263753543479659 ) ) ;
#9341=CARTESIAN_POINT ( 'NONE',  ( 3.510273485745297961, 2.827716139362650427, -3.610536846335888228 ) ) ;
#9346=CARTESIAN_POINT ( 'NONE',  ( -4.154094228333558014, 2.398367420968053221, -3.721909803043253806 ) ) ;
#9368=TOROIDAL_SURFACE ( 'NONE', #952, 5.384454397937118664, 0.5155456020628804703 ) ;
#9394=ADVANCED_FACE ( 'NONE', ( #4647 ), #3680, .T. ) ;
#9429=FACE_OUTER_BOUND ( 'NONE', #3227, .T. ) ;
#9454=VERTEX_POINT ( 'NONE', #2859 ) ;
#9459=ADVANCED_FACE ( 'NONE', ( #7909 ), #959, .T. ) ;
#9464=CARTESIAN_POINT ( 'NONE',  ( -2.000000000000005329, 3.464101615137750390, 1.561251128379126385E-14 ) ) ;
#9479=CARTESIAN_POINT ( 'NONE',  ( 0.000000000000000000, 4.862606272033057841, -3.745885042887454830 ) ) ;
#9481=EDGE_CURVE ( 'NONE', #12721, #7775, #8696, .T. ) ;
#9486=ORIENTED_EDGE ( 'NONE', *, *, #4068, .T. ) ;
#9539=EDGE_LOOP ( 'NONE', ( #1793, #10666, #12009 ) ) ;
#9582=CARTESIAN_POINT ( 'NONE',  ( -4.024497503033700241, -2.323544716729510018, -3.572167766733751915 ) ) ;
#9613=ORIENTED_EDGE ( 'NONE', *, *, #360, .F. ) ;
#9621=ORIENTED_EDGE ( 'NONE', *, *, #2514, .T. ) ;
#9631=STYLED_ITEM ( 'NONE', ( #3971 ), #1664 ) ;
#9634=DIRECTION ( 'NONE',  ( -0.5000000000000019984, -0.8660254037844375974, -2.465190328815657787E-32 ) ) ;
#9641=DIRECTION ( 'NONE',  ( 0.8660254037844379305, 0.5000000000000013323, 0.000000000000000000 ) ) ;
#9648=CIRCLE ( 'NONE', #11529, 2.100000000000000089 ) ;
#9656=CARTESIAN_POINT ( 'NONE',  ( 0.3461262719736449833, -4.658553426539310038, -3.671615880910380270 ) ) ;
#9662=CARTESIAN_POINT ( 'NONE',  ( -4.000000000000012434, 2.309401076758501592, -3.433295621305395340 ) ) ;
#9665=CARTESIAN_POINT ( 'NONE',  ( 2.000000000000010214, -3.464101615137749945, -3.142992957459262549 ) ) ;
#9666=CARTESIAN_POINT ( 'NONE',  ( 4.000000000000000000, -0.3979232138631230709, -2.371692252312040025E-17 ) ) ;
#9670=EDGE_CURVE ( 'NONE', #4184, #12673, #12571, .T. ) ;
#9671=CARTESIAN_POINT ( 'NONE',  ( 4.197393957002303999, 0.8151795401431323196, -3.503767560748939580 ) ) ;
#9674=ORIENTED_EDGE ( 'NONE', *, *, #5441, .F. ) ;
#9678=EDGE_LOOP ( 'NONE', ( #6067, #8966, #12407, #2361, #12683 ) ) ;
#9680=CARTESIAN_POINT ( 'NONE',  ( 0.000000000000000000, 4.618802153516985420, -3.433295621305398893 ) ) ;
#9691=ORIENTED_EDGE ( 'NONE', *, *, #10680, .T. ) ;
#9696=EDGE_LOOP ( 'NONE', ( #2856, #790 ) ) ;
#9713=DIRECTION ( 'NONE',  ( -0.000000000000000000, -1.530455820933490821E-32, 1.000000000000000000 ) ) ;
#9746=CARTESIAN_POINT ( 'NONE',  ( -1.654252653721905331, -3.663718938583013340, -0.01223254789873431253 ) ) ;
#9747=ORIENTED_EDGE ( 'NONE', *, *, #3515, .T. ) ;
#9748=DIRECTION ( 'NONE',  ( 0.000000000000000000, 1.530455820933490821E-32, -1.000000000000000000 ) ) ;
#9780=DIRECTION ( 'NONE',  ( -1.000000000000000000, 1.332267629550187849E-14, 0.000000000000000000 ) ) ;
#9783=CARTESIAN_POINT ( 'NONE',  ( 3.122502256758252770E-14, -4.618802153517026277, -3.504271511727134580 ) ) ;
#9784=CARTESIAN_POINT ( 'NONE',  ( 4.197393957002303999, 7.389034437926038210E-14, -3.503767560748934251 ) ) ;
#9788=LINE ( 'NONE', #11810, #6836 ) ;
#9790=ORIENTED_EDGE ( 'NONE', *, *, #2758, .T. ) ;
#9792=CARTESIAN_POINT ( 'NONE',  ( 4.000000000000000000, -1.942223658245634255, -0.3516579909967644801 ) ) ;
#9796=DIRECTION ( 'NONE',  ( 0.000000000000000000, -1.530455820933490821E-32, 1.000000000000000000 ) ) ;
#9810=CARTESIAN_POINT ( 'NONE',  ( -5.384454397937084025, -2.799244553968360123E-15, -5.000000000000011546 ) ) ;
#9826=CARTESIAN_POINT ( 'NONE',  ( -0.02448733951237958006, -4.877042772274735150, -3.751161874094032012 ) ) ;
#9842=VECTOR ( 'NONE', #10615, 1000.000000000000000 ) ;
#9864=CARTESIAN_POINT ( 'NONE',  ( -5.560781378645556217, -3.469446951953614189E-15, -4.000000000000010658 ) ) ;
#9879=DIRECTION ( 'NONE',  ( 0.000000000000000000, -1.530455820933490821E-32, 1.000000000000000000 ) ) ;
#9889=CARTESIAN_POINT ( 'NONE',  ( 4.211405965630456549, 2.460463115436249293, -3.751298928144576106 ) ) ;
#9892=FACE_OUTER_BOUND ( 'NONE', #2797, .T. ) ;
#9895=CARTESIAN_POINT ( 'NONE',  ( 4.236525694536561026, -2.416953475386480754, -3.751298745799842571 ) ) ;
#9897=EDGE_LOOP ( 'NONE', ( #5910, #4100, #8121, #5233, #2453 ) ) ;
#9909=CIRCLE ( 'NONE', #2124, 2.500000000000000888 ) ;
#9922=DIRECTION ( 'NONE',  ( 1.000000000000000000, 0.000000000000000000, 0.000000000000000000 ) ) ;
#9930=DIRECTION ( 'NONE',  ( 1.000000000000000000, 0.000000000000000000, 0.000000000000000000 ) ) ;
#9961=ORIENTED_EDGE ( 'NONE', *, *, #4360, .T. ) ;
#9974=B_SPLINE_CURVE_WITH_KNOTS ( 'NONE', 3,
 ( #7523, #11460, #2641, #12301, #6561, #10477 ),
 .UNSPECIFIED., .F., .F.,
 ( 4, 2, 4 ),
 ( 0.002365888236227965159, 0.003551327329835074573, 0.004736766423442183988 ),
 .UNSPECIFIED. ) ;
#10005=CARTESIAN_POINT ( 'NONE',  ( 0.000000000000000000, 0.000000000000000000, 0.000000000000000000 ) ) ;
#10010=EDGE_LOOP ( 'NONE', ( #7726, #159, #7262, #6978 ) ) ;
#10015=CARTESIAN_POINT ( 'NONE',  ( 4.000000000000001776, 1.658577278524726584, -3.531553309553335129 ) ) ;
#10038=CARTESIAN_POINT ( 'NONE',  ( 3.472371940586244321, 2.614027278893029660, -3.320322319201107764 ) ) ;
#10048=CARTESIAN_POINT ( 'NONE',  ( -4.211399284164264678, 2.459729995988193973, -3.751162237960548929 ) ) ;
#10075=ORIENTED_EDGE ( 'NONE', *, *, #4542, .F. ) ;
#10081=CARTESIAN_POINT ( 'NONE',  ( 4.000000000000000000, 0.9868501483902617499, -0.09357334158579612426 ) ) ;
#10082=( GEOMETRIC_REPRESENTATION_CONTEXT ( 3 ) GLOBAL_UNCERTAINTY_ASSIGNED_CONTEXT ( ( #6504 ) ) GLOBAL_UNIT_ASSIGNED_CONTEXT ( ( #3934, #447, #11274 ) ) REPRESENTATION_CONTEXT ( 'NONE', 'WORKASPACE' ) );
#10095=CARTESIAN_POINT ( 'NONE',  ( -3.999999999999991562, 0.1981133338132476940, 6.974363408573500627E-15 ) ) ;
#10104=CARTESIAN_POINT ( 'NONE',  ( 2.836893136758657619, 3.208949435745621859, -3.505054077164843740 ) ) ;
#10113=FACE_OUTER_BOUND ( 'NONE', #11986, .T. ) ;
#10141=CARTESIAN_POINT ( 'NONE',  ( -1.287237434361587551, -3.875615274277552036, -3.430618716626829379 ) ) ;
#10145=CARTESIAN_POINT ( 'NONE',  ( -2.000000000000005329, 3.464101615137750390, 1.561251128379126385E-14 ) ) ;
#10146=CARTESIAN_POINT ( 'NONE',  ( -1.747541505913285276, 3.837784562140254430, -3.503702292528920736 ) ) ;
#10156=CARTESIAN_POINT ( 'NONE',  ( 4.000000000000001776, -1.677850389431038591, -3.535268758347268836 ) ) ;
#10162=( BOUNDED_SURFACE ( )  B_SPLINE_SURFACE ( 3, 2, ( 
 ( #8085, #359, #12031 ),
 ( #12163, #3282, #11183 ),
 ( #3222, #8280, #11120 ),
 ( #4288, #8217, #7134 ),
 ( #3342, #11057, #7263 ),
 ( #2372, #6285, #10193 ) ),
 .UNSPECIFIED., .F., .F., .T. ) 
 B_SPLINE_SURFACE_WITH_KNOTS ( ( 4, 2, 4 ),
 ( 3, 3 ),
 ( 0.02032853247518125531, 0.02278863295364820865, 0.02524873343211516200 ),
 ( 0.000000000000000000, 1.000000000000000000 ),
 .UNSPECIFIED. ) 
 GEOMETRIC_REPRESENTATION_ITEM ( )  RATIONAL_B_SPLINE_SURFACE ( (
 ( 1.000000000000000000, 0.8047781615896839602, 1.000000000000000000),
 ( 1.000000000000000000, 0.8123767586288903608, 1.000000000000000000),
 ( 1.000000000000000000, 0.8190662415564864407, 1.000000000000000000),
 ( 1.000000000000000000, 0.8192361015668554458, 1.000000000000000000),
 ( 1.000000000000000000, 0.8126135807104249986, 1.000000000000000000),
 ( 1.000000000000000000, 0.8047712338318581127, 1.000000000000000000) ) ) 
 REPRESENTATION_ITEM ( '' )  SURFACE ( )  );
#10166=EDGE_CURVE ( 'NONE', #2170, #10993, #540, .T. ) ;
#10169=AXIS2_PLACEMENT_3D ( 'NONE', #404, #8324, #1303 ) ;
#10173=CARTESIAN_POINT ( 'NONE',  ( -3.999999999999993339, -1.680117682357838316, -3.316611593219338072 ) ) ;
#10174=CARTESIAN_POINT ( 'NONE',  ( 2.449848172108550326, 3.432307619358736961, -3.503702292528910522 ) ) ;
#10176=CARTESIAN_POINT ( 'NONE',  ( 3.469446951953614189E-14, -3.469446951953614189E-15, -4.484454397937126302 ) ) ;
#10183=EDGE_LOOP ( 'NONE', ( #761, #11257, #8258, #1249 ) ) ;
#10184=CARTESIAN_POINT ( 'NONE',  ( -0.3198814748697738075, -4.434118497892174382, -0.3507732604232444706 ) ) ;
#10185=DIRECTION ( 'NONE',  ( 1.000000000000000000, 0.000000000000000000, 0.000000000000000000 ) ) ;
#10193=CARTESIAN_POINT ( 'NONE',  ( -4.236525694536565467, 2.416953475386456329, -3.751298745799851897 ) ) ;
#10206=CARTESIAN_POINT ( 'NONE',  ( 3.999999999999999112, 1.941961291383485610, -0.3515519931180244861 ) ) ;
#10208=CARTESIAN_POINT ( 'NONE',  ( -4.211140560182161430, -2.431303136016561783, -3.745885042887451277 ) ) ;
#10236=B_SPLINE_CURVE_WITH_KNOTS ( 'NONE', 3,
 ( #3924, #7663, #1861, #11850, #11786, #4891, #10735, #5782 ),
 .UNSPECIFIED., .F., .F.,
 ( 4, 2, 2, 4 ),
 ( 2.465131517071101953E-07, 0.001183067374689835902, 0.001774477805458900314, 0.002365888236227965159 ),
 .UNSPECIFIED. ) ;
#10237=EDGE_CURVE ( 'NONE', #3455, #1611, #11713, .T. ) ;
#10242=VERTEX_POINT ( 'NONE', #5808 ) ;
#10248=VERTEX_POINT ( 'NONE', #8455 ) ;
#10263=ORIENTED_EDGE ( 'NONE', *, *, #11543, .T. ) ;
#10272=DIRECTION ( 'NONE',  ( 1.000000000000000000, 0.000000000000000000, 0.000000000000000000 ) ) ;
#10289=( LENGTH_UNIT ( ) NAMED_UNIT ( * ) SI_UNIT ( .MILLI., .METRE. ) );
#10290=CARTESIAN_POINT ( 'NONE',  ( -4.198928548860765275, 0.8158838809860013974, -3.526471437616931937 ) ) ;
#10295=DIRECTION ( 'NONE',  ( -1.000000000000000000, 0.000000000000000000, 0.000000000000000000 ) ) ;
#10297=CARTESIAN_POINT ( 'NONE',  ( 1.274258131565028762, 3.883108878240869810, -3.220599429844238415 ) ) ;
#10301=CIRCLE ( 'NONE', #1480, 4.000000000000000000 ) ;
#10311=ORIENTED_EDGE ( 'NONE', *, *, #11321, .F. ) ;
#10325=CARTESIAN_POINT ( 'NONE',  ( 4.198928548860774157, -0.8158838809860118335, -3.526471437616922167 ) ) ;
#10344=CARTESIAN_POINT ( 'NONE',  ( -0.3461262719736130089, 4.658553426539255859, -3.671615880910391816 ) ) ;
#10345=DIRECTION ( 'NONE',  ( -1.000000000000000000, 0.000000000000000000, 0.000000000000000000 ) ) ;
#10367=EDGE_CURVE ( 'NONE', #3527, #2170, #9648, .T. ) ;
#10369=ORIENTED_EDGE ( 'NONE', *, *, #5077, .F. ) ;
#10374=CARTESIAN_POINT ( 'NONE',  ( 4.024499207728855055, -2.323545700935701674, -3.572172305156885219 ) ) ;
#10385=VERTEX_POINT ( 'NONE', #7807 ) ;
#10413=B_SPLINE_CURVE_WITH_KNOTS ( 'NONE', 3,
 ( #11000, #7144, #8997, #6041, #10081, #3100, #10206, #5145 ),
 .UNSPECIFIED., .F., .F.,
 ( 4, 2, 2, 4 ),
 ( 0.005725059856848646080, 0.006314084072593635286, 0.006903108288338623624, 0.008081156719828602036 ),
 .UNSPECIFIED. ) ;
#10417=EDGE_CURVE ( 'NONE', #3527, #4184, #12000, .T. ) ;
#10424=CARTESIAN_POINT ( 'NONE',  ( -2.775557561562891351E-14, -4.618802153517012954, -0.5000000000000004441 ) ) ;
#10432=CARTESIAN_POINT ( 'NONE',  ( -0.1756481739660440966, 4.720212674038974932, -3.469390959564073285 ) ) ;
#10434=CARTESIAN_POINT ( 'NONE',  ( 0.000000000000000000, 0.000000000000000000, 0.000000000000000000 ) ) ;
#10441=CARTESIAN_POINT ( 'NONE',  ( 1.654252653721900224, 3.663718938583006235, -0.01223254789872770323 ) ) ;
#10451=CONICAL_SURFACE ( 'NONE', #6346, 4.000000000000000000, 0.8911886515913786111 ) ;
#10468=B_SPLINE_CURVE_WITH_KNOTS ( 'NONE', 3,
 ( #11612, #10507, #11739, #10754, #11675, #3696, #9656, #10693 ),
 .UNSPECIFIED., .F., .F.,
 ( 4, 2, 2, 4 ),
 ( 0.000000000000000000, 0.002450665683189820129, 0.003675998524784730194, 0.004901331366379640259 ),
 .UNSPECIFIED. ) ;
#10477=CARTESIAN_POINT ( 'NONE',  ( -2.775557561562891351E-14, -4.618802153517012954, -0.5000000000000004441 ) ) ;
#10499=CARTESIAN_POINT ( 'NONE',  ( 0.000000000000000000, -4.618802153517027165, -5.000000000000000888 ) ) ;
#10507=CARTESIAN_POINT ( 'NONE',  ( 3.511755186886750923, -2.826662030176405160, -3.597382984111576754 ) ) ;
#10547=CIRCLE ( 'NONE', #6030, 2.100000000000000089 ) ;
#10552=EDGE_CURVE ( 'NONE', #8586, #1828, #4911, .T. ) ;
#10553=CYLINDRICAL_SURFACE ( 'NONE', #10991, 2.100000000000000089 ) ;
#10570=ADVANCED_FACE ( 'NONE', ( #1355 ), #12341, .F. ) ;
#10573=B_SPLINE_CURVE_WITH_KNOTS ( 'NONE', 3,
 ( #12381, #2457, #10290, #3555, #4446, #641 ),
 .UNSPECIFIED., .F., .F.,
 ( 4, 2, 4 ),
 ( 0.002452478801916380645, 0.003676905084148010018, 0.004901331366379639391 ),
 .UNSPECIFIED. ) ;
#10591=AXIS2_PLACEMENT_3D ( 'NONE', #10005, #3976, #6882 ) ;
#10615=DIRECTION ( 'NONE',  ( 0.000000000000000000, -1.530455820933490821E-32, 1.000000000000000000 ) ) ;
#10635=VECTOR ( 'NONE', #295, 1000.000000000000000 ) ;
#10664=VERTEX_POINT ( 'NONE', #1742 ) ;
#10666=ORIENTED_EDGE ( 'NONE', *, *, #6843, .T. ) ;
#10678=DIRECTION ( 'NONE',  ( 1.000000000000000000, 0.000000000000000000, 0.000000000000000000 ) ) ;
#10680=EDGE_CURVE ( 'NONE', #12512, #2523, #4774, .T. ) ;
#10693=CARTESIAN_POINT ( 'NONE',  ( 3.122502256758252770E-14, -4.862606272033112909, -3.745885042887444616 ) ) ;
#10699=CARTESIAN_POINT ( 'NONE',  ( -4.000000000000012434, 1.539600717838998545, -3.300726591567094470 ) ) ;
#10700=COLOUR_RGB ( '', 0.09019608, 0.27058824, 0.51372549) ;
#10703=LINE ( 'NONE', #7044, #11804 ) ;
#10708=CARTESIAN_POINT ( 'NONE',  ( 4.203833317240878387, 1.627343821129577872, -3.597273115243871722 ) ) ;
#10728=EDGE_CURVE ( 'NONE', #8586, #962, #5981, .T. ) ;
#10730=AXIS2_PLACEMENT_3D ( 'NONE', #11419, #903, #4837 ) ;
#10735=CARTESIAN_POINT ( 'NONE',  ( 2.171643655288379104, -3.365003104552334978, -1.177008749073000871E-14 ) ) ;
#10754=CARTESIAN_POINT ( 'NONE',  ( 1.747541505913291937, -3.837784562140264644, -3.503702292528917628 ) ) ;
#10758=ADVANCED_FACE ( 'NONE', ( #11857, #126 ), #8818, .F. ) ;
#10766=CARTESIAN_POINT ( 'NONE',  ( 4.000000000000000000, -2.309401076758518911, -0.4999999999999917843 ) ) ;
#10771=CARTESIAN_POINT ( 'NONE',  ( 4.211140560182196069, 2.431303136016537358, -3.745885042887416638 ) ) ;
#10789=ORIENTED_EDGE ( 'NONE', *, *, #360, .T. ) ;
#10798=B_SPLINE_CURVE_WITH_KNOTS ( 'NONE', 3,
 ( #5362, #720, #3507, #12519, #11360, #10441, #3695, #12264 ),
 .UNSPECIFIED., .F., .F.,
 ( 4, 2, 2, 4 ),
 ( 2.465131517098020131E-07, 0.001183067374689850647, 0.001774477805458922215, 0.002365888236227993349 ),
 .UNSPECIFIED. ) ;
#10820=CARTESIAN_POINT ( 'NONE',  ( -3.999999999999991562, -1.942223658245627149, -0.3516579909967557649 ) ) ;
#10845=FACE_OUTER_BOUND ( 'NONE', #10183, .T. ) ;
#10861=CARTESIAN_POINT ( 'NONE',  ( 0.02511973781851166085, -4.877415612947438639, -3.751298745799855894 ) ) ;
#10870=ORIENTED_EDGE ( 'NONE', *, *, #5441, .T. ) ;
#10905=VERTEX_POINT ( 'NONE', #5581 ) ;
#10908=ORIENTED_EDGE ( 'NONE', *, *, #2270, .F. ) ;
#10915=SURFACE_STYLE_FILL_AREA ( #43 ) ;
#10929=CARTESIAN_POINT ( 'NONE',  ( -1.274258131565009000, -3.883108878240904449, -3.220599429843879147 ) ) ;
#10947=ADVANCED_BREP_SHAPE_REPRESENTATION ( '', ( #1664, #12422 ), #10082 ) ;
#10960=CARTESIAN_POINT ( 'NONE',  ( -3.999999999999993339, 2.511478553582019213, -3.469254451724774757 ) ) ;
#10973=CYLINDRICAL_SURFACE ( 'NONE', #6629, 2.500000000000000444 ) ;
#10976=PRODUCT_CONTEXT ( 'NONE', #409, 'mechanical' ) ;
#10979=ORIENTED_EDGE ( 'NONE', *, *, #2077, .F. ) ;
#10991=AXIS2_PLACEMENT_3D ( 'NONE', #3557, #1738, #12253 ) ;
#10993=VERTEX_POINT ( 'NONE', #11635 ) ;
#11000=CARTESIAN_POINT ( 'NONE',  ( 4.000000000000000000, 0.000000000000000000, 0.000000000000000000 ) ) ;
#11004=CARTESIAN_POINT ( 'NONE',  ( -2.855764796983343956, 2.970025579236416746, -0.09382832055445594621 ) ) ;
#11013=CONICAL_SURFACE ( 'NONE', #6488, 2.059999999999998721, 0.9599310885968738161 ) ;
#11020=B_SPLINE_CURVE_WITH_KNOTS ( 'NONE', 3,
 ( #11661, #5662, #12573, #7667 ),
 .UNSPECIFIED., .F., .F.,
 ( 4, 4 ),
 ( 0.000000000000000000, 0.002452478801916380645 ),
 .UNSPECIFIED. ) ;
#11031=CARTESIAN_POINT ( 'NONE',  ( -4.203934362469355257, -1.640673743454835520, -3.598432614607002034 ) ) ;
#11039=ORIENTED_EDGE ( 'NONE', *, *, #758, .F. ) ;
#11057=CARTESIAN_POINT ( 'NONE',  ( -3.436319922987216557, 2.634841920960315775, -3.531542292955241358 ) ) ;
#11063=CARTESIAN_POINT ( 'NONE',  ( 2.100000000000000089, 0.000000000000000000, -0.2800830152838839626 ) ) ;
#11082=CARTESIAN_POINT ( 'NONE',  ( -3.679171394226032454, -2.494631558665832305, -0.3503314178412488822 ) ) ;
#11097=CARTESIAN_POINT ( 'NONE',  ( -3.999999999999993339, 0.8576368993457464951, -3.433240632782212032 ) ) ;
#11120=CARTESIAN_POINT ( 'NONE',  ( -1.360585162435275164, 4.061296242128064726, -3.505054077164865500 ) ) ;
#11128=DIRECTION ( 'NONE',  ( 0.000000000000000000, 1.530455820933490821E-32, -1.000000000000000000 ) ) ;
#11129=CARTESIAN_POINT ( 'NONE',  ( 0.000000000000000000, 0.000000000000000000, 3.469446951953614189E-15 ) ) ;
#11145=ADVANCED_FACE ( 'NONE', ( #10845 ), #10973, .F. ) ;
#11151=CARTESIAN_POINT ( 'NONE',  ( 4.000000000000001776, -2.511475576507302687, -3.469253905236651558 ) ) ;
#11169=EDGE_CURVE ( 'NONE', #1828, #3396, #1208, .T. ) ;
#11176=ORIENTED_EDGE ( 'NONE', *, *, #7732, .F. ) ;
#11183=CARTESIAN_POINT ( 'NONE',  ( -0.6640947660594385127, 4.471078309994347855, -3.602146406945782253 ) ) ;
#11199=CARTESIAN_POINT ( 'NONE',  ( -3.510273485745275313, -2.827716139362673964, -3.610536846335894889 ) ) ;
#11234=EDGE_CURVE ( 'NONE', #4694, #1828, #8988, .T. ) ;
#11237=CARTESIAN_POINT ( 'NONE',  ( -4.101948962586056346, 2.368261337751164763, -3.681124513963754730 ) ) ;
#11257=ORIENTED_EDGE ( 'NONE', *, *, #3563, .T. ) ;
#11274=( NAMED_UNIT ( * ) SI_UNIT ( $, .STERADIAN. ) SOLID_ANGLE_UNIT ( ) );
#11296=CIRCLE ( 'NONE', #11507, 0.5155456020628804703 ) ;
#11305=CARTESIAN_POINT ( 'NONE',  ( 0.000000000000000000, 0.000000000000000000, -0.2800830152838839626 ) ) ;
#11321=EDGE_CURVE ( 'NONE', #38, #3396, #5007, .T. ) ;
#11350=CARTESIAN_POINT ( 'NONE',  ( 1.390230914382213800, 4.043987460488878583, -3.502507215260568962 ) ) ;
#11360=CARTESIAN_POINT ( 'NONE',  ( 1.312671235360366895, 3.860931062424212801, -0.05923475698269817236 ) ) ;
#11364=VECTOR ( 'NONE', #2131, 1000.000000000000000 ) ;
#11393=VERTEX_POINT ( 'NONE', #11495 ) ;
#11396=DIRECTION ( 'NONE',  ( -1.000000000000000000, 0.000000000000000000, 0.000000000000000000 ) ) ;
#11398=DIRECTION ( 'NONE',  ( 0.000000000000000000, -1.530455820933490821E-32, 1.000000000000000000 ) ) ;
#11414=DIRECTION ( 'NONE',  ( 0.000000000000000000, 1.530455820933490821E-32, -1.000000000000000000 ) ) ;
#11419=CARTESIAN_POINT ( 'NONE',  ( 0.000000000000000000, -3.469446951953614189E-14, -25.03750572909320837 ) ) ;
#11434=CIRCLE ( 'NONE', #8345, 4.000000000000000000 ) ;
#11460=CARTESIAN_POINT ( 'NONE',  ( 1.655952806101427699, -3.662737355149048746, -1.169794851805551168E-14 ) ) ;
#11485=CARTESIAN_POINT ( 'NONE',  ( 4.000000000000001776, -1.539567084929416296E-14, -3.142992957459251890 ) ) ;
#11495=CARTESIAN_POINT ( 'NONE',  ( -2.499999999999966249, -3.469446951953614189E-15, -4.974600000000009459 ) ) ;
#11507=AXIS2_PLACEMENT_3D ( 'NONE', #7081, #2185, #2121 ) ;
#11529=AXIS2_PLACEMENT_3D ( 'NONE', #3121, #2211, #7926 ) ;
#11543=EDGE_CURVE ( 'NONE', #3396, #2015, #4389, .T. ) ;
#11568=EDGE_CURVE ( 'NONE', #4184, #7175, #9788, .T. ) ;
#11601=ORIENTED_EDGE ( 'NONE', *, *, #3289, .T. ) ;
#11612=CARTESIAN_POINT ( 'NONE',  ( 4.211140560182228043, -2.431303136016558231, -3.745885042887437510 ) ) ;
#11623=ORIENTED_EDGE ( 'NONE', *, *, #1228, .F. ) ;
#11625=CARTESIAN_POINT ( 'NONE',  ( 4.000000000000000000, 0.000000000000000000, 0.000000000000000000 ) ) ;
#11629=FACE_OUTER_BOUND ( 'NONE', #5772, .T. ) ;
#11635=CARTESIAN_POINT ( 'NONE',  ( 2.500000000000035527, -3.163285252166775924E-15, -4.974600000000009459 ) ) ;
#11639=EDGE_CURVE ( 'NONE', #3527, #11393, #3190, .T. ) ;
#11646=DIRECTION ( 'NONE',  ( -0.000000000000000000, -1.530455820933490821E-32, 1.000000000000000000 ) ) ;
#11661=CARTESIAN_POINT ( 'NONE',  ( -4.211140560182161430, -2.431303136016561783, -3.745885042887451277 ) ) ;
#11664=CARTESIAN_POINT ( 'NONE',  ( 4.024499207728844397, 2.323545700935675473, -3.572172305156859462 ) ) ;
#11675=CARTESIAN_POINT ( 'NONE',  ( 1.393927851585494260, -4.043713361053535849, -3.526374918436848027 ) ) ;
#11680=DIRECTION ( 'NONE',  ( 1.000000000000000000, 0.000000000000000000, 0.000000000000000000 ) ) ;
#11689=DIRECTION ( 'NONE',  ( 1.000000000000000000, 0.000000000000000000, 0.000000000000000000 ) ) ;
#11692=VERTEX_POINT ( 'NONE', #1944 ) ;
#11713=CIRCLE ( 'NONE', #6778, 5.384454397937118664 ) ;
#11722=VECTOR ( 'NONE', #7103, 1000.000000000000000 ) ;
#11739=CARTESIAN_POINT ( 'NONE',  ( 2.805705207896072029, -3.226868319750169967, -3.503898532754375239 ) ) ;
#11740=CARTESIAN_POINT ( 'NONE',  ( -3.999999999999994671, -2.309401076758511806, -0.4999999999999865663 ) ) ;
#11748=B_SPLINE_CURVE_WITH_KNOTS ( 'NONE', 3,
 ( #5254, #2498, #10325, #2238, #9296, #487 ),
 .UNSPECIFIED., .F., .F.,
 ( 4, 2, 4 ),
 ( 0.002452478801916361563, 0.003676905084148001344, 0.004901331366379641126 ),
 .UNSPECIFIED. ) ;
#11786=CARTESIAN_POINT ( 'NONE',  ( 2.687328764639645762, -3.067272167851298192, -0.05923475698271467305 ) ) ;
#11797=AXIS2_PLACEMENT_3D ( 'NONE', #9290, #4547, #2617 ) ;
#11803=CARTESIAN_POINT ( 'NONE',  ( 3.469446951953614189E-14, -3.469446951953614189E-15, -4.974600000000009459 ) ) ;
#11804=VECTOR ( 'NONE', #4981, 1000.000000000000000 ) ;
#11807=CARTESIAN_POINT ( 'NONE',  ( 3.469446951953614189E-14, -3.469446951953614189E-15, -4.974600000000009459 ) ) ;
#11810=CARTESIAN_POINT ( 'NONE',  ( -2.059999999999998721, 2.522772406243545965E-16, -0.3080913168122742518 ) ) ;
#11811=AXIS2_PLACEMENT_3D ( 'NONE', #2253, #438, #8294 ) ;
#11813=EDGE_LOOP ( 'NONE', ( #1834, #1719, #2339, #7710 ) ) ;
#11840=VECTOR ( 'NONE', #11398, 1000.000000000000000 ) ;
#11842=EDGE_CURVE ( 'NONE', #8996, #2015, #1300, .T. ) ;
#11850=CARTESIAN_POINT ( 'NONE',  ( 2.855764796983347065, -2.970025579236429181, -0.09382832055446509167 ) ) ;
#11855=AXIS2_PLACEMENT_3D ( 'NONE', #11129, #115, #9060 ) ;
#11857=FACE_BOUND ( 'NONE', #9696, .T. ) ;
#11877=EDGE_CURVE ( 'NONE', #529, #10242, #10301, .T. ) ;
#11888=B_SPLINE_CURVE_WITH_KNOTS ( 'NONE', 3,
 ( #10766, #9792, #7693, #25, #9666, #11625 ),
 .UNSPECIFIED., .F., .F.,
 ( 4, 2, 4 ),
 ( 0.003358874760055554493, 0.004541967308452099852, 0.005725059856848646080 ),
 .UNSPECIFIED. ) ;
#11904=VERTEX_POINT ( 'NONE', #12639 ) ;
#11927=VECTOR ( 'NONE', #595, 1000.000000000000114 ) ;
#11930=CARTESIAN_POINT ( 'NONE',  ( -2.805705207896076914, 3.226868319750153535, -3.503898532754382344 ) ) ;
#11952=ADVANCED_FACE ( 'NONE', ( #7481 ), #4708, .F. ) ;
#11955=ORIENTED_EDGE ( 'NONE', *, *, #11639, .F. ) ;
#11986=EDGE_LOOP ( 'NONE', ( #4821, #6006, #308 ) ) ;
#12000=LINE ( 'NONE', #4847, #11722 ) ;
#12009=ORIENTED_EDGE ( 'NONE', *, *, #4033, .F. ) ;
#12011=B_SPLINE_CURVE_WITH_KNOTS ( 'NONE', 3,
 ( #76, #4129, #8047, #4973, #11082, #6969 ),
 .UNSPECIFIED., .F., .F.,
 ( 4, 2, 4 ),
 ( 0.002365888236228003323, 0.003551327329835090186, 0.004736766423442177049 ),
 .UNSPECIFIED. ) ;
#12014=CIRCLE ( 'NONE', #11811, 5.560781378645573980 ) ;
#12031=CARTESIAN_POINT ( 'NONE',  ( 0.02448733951238716428, 4.877042772274719162, -3.751161874094028903 ) ) ;
#12042=CARTESIAN_POINT ( 'NONE',  ( -0.6810597143199018655, -4.461075778259501412, -3.598441714920685541 ) ) ;
#12089=EDGE_CURVE ( 'NONE', #2015, #11692, #4901, .T. ) ;
#12104=CARTESIAN_POINT ( 'NONE',  ( -2.836893136758698031, -3.208949435745759970, -3.505054077164898807 ) ) ;
#12109=B_SPLINE_CURVE_WITH_KNOTS ( 'NONE', 3,
 ( #8018, #10184, #1380, #5310, #4347, #9746, #12485, #5833 ),
 .UNSPECIFIED., .F., .F.,
 ( 4, 2, 2, 4 ),
 ( 2.465131517396146612E-07, 0.001183067374689870379, 0.001774477805458936960, 0.002365888236228003323 ),
 .UNSPECIFIED. ) ;
#12119=SHAPE_REPRESENTATION_RELATIONSHIP ( 'NONE' , 'NONE' ,  #9199, #10947 ) ;
#12122=DIRECTION ( 'NONE',  ( -1.000000000000000000, 0.000000000000000000, 0.000000000000000000 ) ) ;
#12139=CARTESIAN_POINT ( 'NONE',  ( -4.211405944401390933, -2.460460786169392566, -3.751298493805505174 ) ) ;
#12163=CARTESIAN_POINT ( 'NONE',  ( -0.5276280594147285674, 4.314175951381911567, -3.320322319201698846 ) ) ;
#12169=ORIENTED_EDGE ( 'NONE', *, *, #11842, .T. ) ;
#12177=CARTESIAN_POINT ( 'NONE',  ( -2.345747346278108658, 3.264484291692490547, -0.01223254789873496305 ) ) ;
#12178=CARTESIAN_POINT ( 'NONE',  ( -3.511755186886760693, 2.826662030176358087, -3.597382984111575421 ) ) ;
#12181=ORIENTED_EDGE ( 'NONE', *, *, #8794, .F. ) ;
#12186=CARTESIAN_POINT ( 'NONE',  ( -3.999999999999992450, 1.563622288139195682, -0.2253451193528239471 ) ) ;
#12234=ORIENTED_EDGE ( 'NONE', *, *, #11877, .F. ) ;
#12249=PRODUCT_DEFINITION_SHAPE ( 'NONE', 'NONE',  #9002 ) ;
#12253=DIRECTION ( 'NONE',  ( 1.000000000000000000, 0.000000000000000000, 0.000000000000000000 ) ) ;
#12264=CARTESIAN_POINT ( 'NONE',  ( 2.000000000000007105, 3.464101615137750390, 6.938893903907228378E-15 ) ) ;
#12283=AXIS2_PLACEMENT_3D ( 'NONE', #7996, #2152, #9922 ) ;
#12301=CARTESIAN_POINT ( 'NONE',  ( 0.6507732100473474501, -4.243078065514793273, -0.2236248678334946949 ) ) ;
#12341=( BOUNDED_SURFACE ( )  B_SPLINE_SURFACE ( 3, 2, ( 
 ( #394, #6192, #458 ),
 ( #10038, #9330, #4390 ),
 ( #7167, #6385, #10104 ),
 ( #10297, #524, #11350 ),
 ( #1486, #4454, #2534 ),
 ( #10432, #3806, #6585 ) ),
 .UNSPECIFIED., .F., .F., .T. ) 
 B_SPLINE_SURFACE_WITH_KNOTS ( ( 4, 2, 4 ),
 ( 3, 3 ),
 ( 0.02032853247518126225, 0.02278863295364821212, 0.02524873343211516200 ),
 ( 0.000000000000000000, 1.000000000000000000 ),
 .UNSPECIFIED. ) 
 GEOMETRIC_REPRESENTATION_ITEM ( )  RATIONAL_B_SPLINE_SURFACE ( (
 ( 1.000000000000000000, 0.8047781615896835161, 1.000000000000000000),
 ( 1.000000000000000000, 0.8123767586289977194, 1.000000000000000000),
 ( 1.000000000000000000, 0.8190662415563441101, 1.000000000000000000),
 ( 1.000000000000000000, 0.8192361015669979984, 1.000000000000000000),
 ( 1.000000000000000000, 0.8126135807103183062, 1.000000000000000000),
 ( 1.000000000000000000, 0.8047712338318581127, 1.000000000000000000) ) ) 
 REPRESENTATION_ITEM ( '' )  SURFACE ( )  );
#12380=B_SPLINE_CURVE_WITH_KNOTS ( 'NONE', 3,
 ( #10771, #10708, #9671, #2016 ),
 .UNSPECIFIED., .F., .F.,
 ( 4, 4 ),
 ( 0.000000000000000000, 0.002452478801916361563 ),
 .UNSPECIFIED. ) ;
#12381=CARTESIAN_POINT ( 'NONE',  ( -4.197393957002295117, -8.025123413315649349E-14, -3.503767560748944021 ) ) ;
#12407=ORIENTED_EDGE ( 'NONE', *, *, #4542, .T. ) ;
#12422=AXIS2_PLACEMENT_3D ( 'NONE', #5707, #7392, #6428 ) ;
#12450=AXIS2_PLACEMENT_3D ( 'NONE', #6300, #4304, #439 ) ;
#12457=CIRCLE ( 'NONE', #2161, 4.000000000000000000 ) ;
#12481=ORIENTED_EDGE ( 'NONE', *, *, #7230, .T. ) ;
#12485=CARTESIAN_POINT ( 'NONE',  ( -1.828356344711643322, -3.563200125723179568, -4.514685608865420807E-16 ) ) ;
#12504=PRODUCT_DEFINITION_FORMATION_WITH_SPECIFIED_SOURCE ( 'ANY', '', #7209, .NOT_KNOWN. ) ;
#12512=VERTEX_POINT ( 'NONE', #7901 ) ;
#12519=CARTESIAN_POINT ( 'NONE',  ( 1.144235203016661595, 3.958177651039084921, -0.09382832055444986774 ) ) ;
#12523=CARTESIAN_POINT ( 'NONE',  ( 0.000000000000000000, 4.618802153517012954, -5.000000000000018652 ) ) ;
#12532=ADVANCED_FACE ( 'NONE', ( #176 ), #4889, .T. ) ;
#12537=ORIENTED_EDGE ( 'NONE', *, *, #10166, .T. ) ;
#12539=DIRECTION ( 'NONE',  ( -1.000000000000000000, 0.000000000000000000, 0.000000000000000000 ) ) ;
#12571=CIRCLE ( 'NONE', #4748, 2.100000000000000089 ) ;
#12573=CARTESIAN_POINT ( 'NONE',  ( -4.197393957002295117, -0.8151795401431458643, -3.503767560748948906 ) ) ;
#12631=ADVANCED_FACE ( 'NONE', ( #1396 ), #7465, .F. ) ;
#12639=CARTESIAN_POINT ( 'NONE',  ( -4.197393957002295117, -8.025123413315649349E-14, -3.503767560748944021 ) ) ;
#12642=DIRECTION ( 'NONE',  ( 0.8191520442889875797, -8.778333957637558005E-33, 0.5735764363510522656 ) ) ;
#12660=CARTESIAN_POINT ( 'NONE',  ( 3.333333333333355242, -2.694301256218273988, -3.300726591567069601 ) ) ;
#12673=VERTEX_POINT ( 'NONE', #11063 ) ;
#12683=ORIENTED_EDGE ( 'NONE', *, *, #758, .T. ) ;
#12699=CARTESIAN_POINT ( 'NONE',  ( -0.1404048886732668089, -4.699864953788076782, -3.686887068327048045 ) ) ;
#12708=LINE ( 'NONE', #4057, #4948 ) ;
#12721=VERTEX_POINT ( 'NONE', #2567 ) ;
ENDSEC;
END-ISO-10303-21;
